ISO-10303-21;
HEADER;
FILE_DESCRIPTION (('STEP AP214'),
    '1' );
FILE_NAME ('Slewing Ring High Pressure Lip Seals Top.step',
    '2026-10-09T12:49:55',
    ( '' ),
    ( '' ),
    'SwSTEP 2.0',
    'SolidWorks 2026',
    '' );
FILE_SCHEMA (( 'AUTOMOTIVE_DESIGN' ));
ENDSEC;

DATA;
#11=CARTESIAN_POINT ( 'NONE',  ( -34.18476129408180242, 19.96883745937779864, 259.4723857443443080 ) ) ;
#12=DIRECTION ( 'NONE',  ( 0.000000000000000000, -1.000000000000000000, 0.000000000000000000 ) ) ;
#17=CARTESIAN_POINT ( 'NONE',  ( 17.06760680892275062, 20.79694577654979071, 260.7745447056980197 ) ) ;
#30=CARTESIAN_POINT ( 'NONE',  ( -247.8175805190998062, 19.96883746075563693, 84.14846197946620521 ) ) ;
#38=CARTESIAN_POINT ( 'NONE',  ( 206.9952515782970295, 20.79694577634646535, 158.8368823490022237 ) ) ;
#48=SURFACE_SIDE_STYLE ('',( #1037 ) ) ;
#51=CARTESIAN_POINT ( 'NONE',  ( 6.345753394971347358E-13, 20.08915143297736350, -260.5542428351130866 ) ) ;
#53=CARTESIAN_POINT ( 'NONE',  ( -137.7829567244536122, 20.79694577634646890, 221.5672498511017920 ) ) ;
#67=CARTESIAN_POINT ( 'NONE',  ( 84.02568524182660781, 20.79694577630801078, -247.4557548099990072 ) ) ;
#80=CARTESIAN_POINT ( 'NONE',  ( 247.2466869557899827, 20.08915143289970473, -83.95474316006121285 ) ) ;
#85=CARTESIAN_POINT ( 'NONE',  ( -1.010328782420808020E-12, 20.79694577634649022, 260.7745447061710138 ) ) ;
#90=VERTEX_POINT ( 'NONE', #9222 ) ;
#97=DIRECTION ( 'NONE',  ( 0.000000000000000000, 0.000000000000000000, -1.000000000000000000 ) ) ;
#99=CARTESIAN_POINT ( 'NONE',  ( 34.18476129334108293, 19.96883746037050855, -259.4723857425807978 ) ) ;
#126=ORIENTED_EDGE ( 'NONE', *, *, #7506, .T. ) ;
#130=CARTESIAN_POINT ( 'NONE',  ( 67.47543992452018813, 20.08915143297736705, -251.8100110699623713 ) ) ;
#132=CARTESIAN_POINT ( 'NONE',  ( 252.4341100445949735, 20.79694577582237613, 67.61424742981928659 ) ) ;
#145=CARTESIAN_POINT ( 'NONE',  ( -172.1812796679919870, 20.08915143287683591, 196.2980642839890209 ) ) ;
#162=CARTESIAN_POINT ( 'NONE',  ( -172.5787240293117293, 19.96883745935916821, -196.7513681803530403 ) ) ;
#164=LINE ( 'NONE', #1161, #5159 ) ;
#168=CARTESIAN_POINT ( 'NONE',  ( 158.8368823490023374, 20.79694577634646535, 206.9952515782968874 ) ) ;
#174=DIRECTION ( 'NONE',  ( 0.000000000000000000, -1.000000000000000000, 0.000000000000000000 ) ) ;
#179=CARTESIAN_POINT ( 'NONE',  ( -206.8203823583188807, 20.08915143297736705, -158.7026972336036295 ) ) ;
#190=VECTOR ( 'NONE', #5245, 1000.000000000000000 ) ;
#193=CARTESIAN_POINT ( 'NONE',  ( 252.4341100441809829, 20.79694577595645910, -67.61424743030308093 ) ) ;
#202=CARTESIAN_POINT ( 'NONE',  ( 84.02568524192950861, 20.79694577611522632, 247.4557548104415048 ) ) ;
#205=CARTESIAN_POINT ( 'NONE',  ( 258.8746690706130380, 20.08915143329827657, -34.10614053547809732 ) ) ;
#213=DIRECTION ( 'NONE',  ( 0.000000000000000000, 0.000000000000000000, -1.000000000000000000 ) ) ;
#220=CYLINDRICAL_SURFACE ( 'NONE', #828, 246.0000000000000000 ) ;
#225=CARTESIAN_POINT ( 'NONE',  ( -252.9796497735838443, 20.55460285104794949, 67.76049180365761515 ) ) ;
#269=CARTESIAN_POINT ( 'NONE',  ( 172.1812796672219861, 20.08915143311016749, 196.2980642831085163 ) ) ;
#275=CARTESIAN_POINT ( 'NONE',  ( 3.077430737863366313E-14, 21.94174202707280941, -251.2912898646363828 ) ) ;
#289=ORIENTED_EDGE ( 'NONE', *, *, #5424, .F. ) ;
#296=CARTESIAN_POINT ( 'NONE',  ( 196.7513681799458709, 19.96883746115198122, -172.5787240287706936 ) ) ;
#302=CARTESIAN_POINT ( 'NONE',  ( -67.53249125288922983, 20.79694577634646890, 252.0229195836990925 ) ) ;
#304=CARTESIAN_POINT ( 'NONE',  ( 247.0684411393755795, 20.79694577634646535, 83.86521783953200782 ) ) ;
#307=ORIENTED_EDGE ( 'NONE', *, *, #6492, .F. ) ;
#324=DIRECTION ( 'NONE',  ( 0.000000000000000000, 0.000000000000000000, -1.000000000000000000 ) ) ;
#326=CARTESIAN_POINT ( 'NONE',  ( 257.2112267038638151, 20.08915143297735995, 42.46883004693714980 ) ) ;
#335=PRODUCT_CONTEXT ( 'NONE', #2943, 'mechanical' ) ;
#341=CARTESIAN_POINT ( 'NONE',  ( 226.6392846536925276, 19.96883745972948176, 130.8783844628973441 ) ) ;
#358=CARTESIAN_POINT ( 'NONE',  ( -196.8887528216966132, 20.55460285140358678, -172.6991790949711287 ) ) ;
#365=CARTESIAN_POINT ( 'NONE',  ( 190.4297758776779688, 20.79694577634647246, -178.3611219674584163 ) ) ;
#386=CARTESIAN_POINT ( 'NONE',  ( 178.2104428091929265, 20.08915143297737060, -190.2689011420770271 ) ) ;
#391=( GEOMETRIC_REPRESENTATION_CONTEXT ( 3 ) GLOBAL_UNCERTAINTY_ASSIGNED_CONTEXT ( ( #7955 ) ) GLOBAL_UNIT_ASSIGNED_CONTEXT ( ( #11965, #7032, #5022 ) ) REPRESENTATION_CONTEXT ( 'NONE', 'WORKASPACE' ) );
#402=CARTESIAN_POINT ( 'NONE',  ( -34.20858920445061102, 20.55460285115536934, 259.6535381498995321 ) ) ;
#406=CARTESIAN_POINT ( 'NONE',  ( -258.4638482596386098, 20.08915143297736705, 34.02434144668497851 ) ) ;
#423=CARTESIAN_POINT ( 'NONE',  ( 130.8783844624215931, 19.96883746229290679, 226.6392846534563716 ) ) ;
#432=CARTESIAN_POINT ( 'NONE',  ( 91.90986972409962164, 20.79694577634646535, -244.1900186690935470 ) ) ;
#439=PRODUCT ( 'Slewing Ring High Pressure Lip Seals Top', 'Slewing Ring High Pressure Lip Seals Top', '', ( #335 ) ) ;
#453=AXIS2_PLACEMENT_3D ( 'NONE', #11170, #7172, #2039 ) ;
#458=AXIS2_PLACEMENT_3D ( 'NONE', #522, #1584, #5646 ) ;
#469=CARTESIAN_POINT ( 'NONE',  ( -130.8783844626380812, 19.96883746054828279, -226.6392846538615231 ) ) ;
#475=CARTESIAN_POINT ( 'NONE',  ( -17.05322212017849282, 20.08915143297736705, 260.1353576186480154 ) ) ;
#491=CARTESIAN_POINT ( 'NONE',  ( 252.9796497720284094, 20.55460285130353881, -67.76049180262273808 ) ) ;
#495=CARTESIAN_POINT ( 'NONE',  ( -225.9597979674043415, 20.79694577634646535, -130.4544329367272724 ) ) ;
#498=CARTESIAN_POINT ( 'NONE',  ( 260.3553053170167004, 20.79694577634646535, -17.06764083276446087 ) ) ;
#520=DIRECTION ( 'NONE',  ( 0.000000000000000000, -1.000000000000000000, 0.000000000000000000 ) ) ;
#522=CARTESIAN_POINT ( 'NONE',  ( 0.000000000000000000, 19.00000000000000000, 250.7029414592220178 ) ) ;
#536=CARTESIAN_POINT ( 'NONE',  ( -226.6392846536229229, 19.96883746130017911, -130.8783844628770794 ) ) ;
#537=ADVANCED_FACE ( 'NONE', ( #2993 ), #3527, .T. ) ;
#556=CARTESIAN_POINT ( 'NONE',  ( 226.7975291061089820, 20.55460285063310621, -130.9697226050975019 ) ) ;
#594=CARTESIAN_POINT ( 'NONE',  ( 115.7315435902013263, 19.96883745981483926, -234.7354397754176318 ) ) ;
#595=CARTESIAN_POINT ( 'NONE',  ( 0.000000000000000000, 24.75600756274008063, -251.5674242726970817 ) ) ;
#617=CARTESIAN_POINT ( 'NONE',  ( -1.009183486025028462E-12, 20.55460285106647689, 261.3381329044966606 ) ) ;
#630=CARTESIAN_POINT ( 'NONE',  ( 137.6665579279354006, 20.08915143297736350, 221.3800702329288299 ) ) ;
#634=DIRECTION ( 'NONE',  ( 0.000000000000000000, 0.000000000000000000, 1.000000000000000000 ) ) ;
#635=FACE_OUTER_BOUND ( 'NONE', #6751, .T. ) ;
#641=DIRECTION ( 'NONE',  ( 0.000000000000000000, -1.000000000000000000, 0.000000000000000000 ) ) ;
#664=CARTESIAN_POINT ( 'NONE',  ( -261.3381329044966606, 20.55460285116648933, 17.10461161605900671 ) ) ;
#684=CARTESIAN_POINT ( 'NONE',  ( -84.02568524195829980, 20.79694577620390916, -247.4557548102065141 ) ) ;
#697=CARTESIAN_POINT ( 'NONE',  ( 8.526617657838038156, 20.08915143297736705, 260.5542428351132571 ) ) ;
#705=CARTESIAN_POINT ( 'NONE',  ( -260.5542428355875018, 20.08915143288246696, -17.05314194217034895 ) ) ;
#716=CLOSED_SHELL ( 'NONE', ( #9981, #4280, #9611, #8563, #12138, #8414, #2407, #1922, #2600, #9168, #537, #7337, #9303, #5842 ) ) ;
#724=CARTESIAN_POINT ( 'NONE',  ( -59.24444182677445525, 20.79694577634646180, -254.0989678903617914 ) ) ;
#735=CARTESIAN_POINT ( 'NONE',  ( -234.8993005735983104, 20.55460285152947009, -115.8123742918138248 ) ) ;
#756=CARTESIAN_POINT ( 'NONE',  ( 84.20717312394452847, 20.55460285104429019, 247.9906035367661161 ) ) ;
#770=CARTESIAN_POINT ( 'NONE',  ( -207.1687172315079692, 20.08915143295307004, 158.9353507253535156 ) ) ;
#774=DIRECTION ( 'NONE',  ( 0.000000000000000000, 0.000000000000000000, -1.000000000000000000 ) ) ;
#780=FACE_BOUND ( 'NONE', #6237, .T. ) ;
#785=CARTESIAN_POINT ( 'NONE',  ( -107.6783259591024944, 20.79694577634646535, -237.6585102388689279 ) ) ;
#794=CARTESIAN_POINT ( 'NONE',  ( 115.8123742916068295, 20.55460285108873819, 234.8993005735927966 ) ) ;
#805=AXIS2_PLACEMENT_3D ( 'NONE', #6711, #10765, #10635 ) ;
#811=CARTESIAN_POINT ( 'NONE',  ( 234.3927740976959910, 20.79694577647348908, -115.5625104414818054 ) ) ;
#821=EDGE_LOOP ( 'NONE', ( #12068, #9534, #10619, #12082 ) ) ;
#828=AXIS2_PLACEMENT_3D ( 'NONE', #12222, #3075, #11213 ) ;
#834=B_SPLINE_CURVE_WITH_KNOTS ( 'NONE', 3,
 ( #11246, #10244, #7057, #12188, #6062, #1121, #130, #4179, #2307, #3365, #2617, #7449, #4379, #10375, #11523, #5386, #386, #12513, #10516, #1386, #2380, #2250, #4680, #8826, #6455, #8521, #5449, #4436, #8392, #9511, #6389, #10449, #9386, #9454, #6704, #12581, #326, #2676, #6765, #3435, #8460, #7517, #1693, #11766, #1319, #5690, #12454, #7321, #10756, #5761, #1624, #3687, #9743, #630, #8757, #12820, #7384, #10819, #3306, #7758, #4749, #11833, #1249, #9819, #697, #12889 ),
 .UNSPECIFIED., .F., .F.,
 ( 4, 2, 2, 2, 2, 2, 2, 2, 2, 2, 2, 2, 2, 2, 2, 2, 2, 2, 2, 2, 2, 2, 2, 2, 2, 2, 2, 2, 2, 2, 2, 2, 4 ),
 ( 0.5000000000000000000, 0.5156250000000000000, 0.5312499999999998890, 0.5468749999999998890, 0.5624999999999998890, 0.5781249999999997780, 0.5937499999999997780, 0.6093749999999997780, 0.6249999999999997780, 0.6406249999999997780, 0.6562499999999997780, 0.6718749999999997780, 0.6874999999999997780, 0.7031249999999997780, 0.7187499999999997780, 0.7343749999999996669, 0.7499999999999997780, 0.7656249999999997780, 0.7812499999999997780, 0.7968749999999997780, 0.8124999999999997780, 0.8281249999999997780, 0.8437499999999997780, 0.8593749999999997780, 0.8749999999999997780, 0.8906249999999998890, 0.9062499999999998890, 0.9218749999999998890, 0.9375000000000000000, 0.9531250000000000000, 0.9687500000000000000, 0.9843750000000000000, 1.000000000000000000 ),
 .UNSPECIFIED. ) ;
#860=CARTESIAN_POINT ( 'NONE',  ( -259.6535381480032356, 20.55460285108499008, 34.20858920320377905 ) ) ;
#879=CIRCLE ( 'NONE', #6214, 251.2912898646364397 ) ;
#896=CARTESIAN_POINT ( 'NONE',  ( -247.8175805188620018, 19.96883746128897386, -84.14846197934974725 ) ) ;
#929=CARTESIAN_POINT ( 'NONE',  ( -1.010328782420808020E-12, 20.79694577634649022, 260.7745447061710138 ) ) ;
#942=ORIENTED_EDGE ( 'NONE', *, *, #8746, .F. ) ;
#953=VERTEX_POINT ( 'NONE', #595 ) ;
#963=CARTESIAN_POINT ( 'NONE',  ( 247.2466869560049929, 20.08915143286045790, 83.95474316005440585 ) ) ;
#990=CARTESIAN_POINT ( 'NONE',  ( 34.13493237066314379, 20.79694577651677889, -259.0935598596149703 ) ) ;
#1003=CARTESIAN_POINT ( 'NONE',  ( -17.09264059776470290, 19.96883746054087538, 261.1558126970361400 ) ) ;
#1007=CARTESIAN_POINT ( 'NONE',  ( 207.3438552934050279, 20.79694577613707551, 159.0697709850429931 ) ) ;
#1011=CARTESIAN_POINT ( 'NONE',  ( 3.073863465859856636E-14, 24.99999999999995737, 251.0000000000000000 ) ) ;
#1022=CARTESIAN_POINT ( 'NONE',  ( 196.2980642840460064, 20.08915143284461280, 172.1812796681624889 ) ) ;
#1028=CARTESIAN_POINT ( 'NONE',  ( 254.0989678903617346, 20.79694577634646890, 59.24444182677502369 ) ) ;
#1037=SURFACE_STYLE_FILL_AREA ( #1733 ) ;
#1041=CARTESIAN_POINT ( 'NONE',  ( -221.3800702329286594, 20.08915143297736705, -137.6665579279355711 ) ) ;
#1044=CARTESIAN_POINT ( 'NONE',  ( -237.6585102388685584, 20.79694577634646535, -107.6783259591029918 ) ) ;
#1054=CARTESIAN_POINT ( 'NONE',  ( 172.3268284095375122, 20.79694577629726027, -196.4640694357605071 ) ) ;
#1068=CARTESIAN_POINT ( 'NONE',  ( 115.4648407707963997, 20.08915143305429041, -234.1947771728865177 ) ) ;
#1073=CARTESIAN_POINT ( 'NONE',  ( 196.4640694362159934, 20.79694577623644491, 172.3268284092819727 ) ) ;
#1089=CARTESIAN_POINT ( 'NONE',  ( -67.71318189764485851, 19.96883746024804651, -252.8031682270704437 ) ) ;
#1097=CIRCLE ( 'NONE', #11097, 250.7029414592220178 ) ;
#1110=CARTESIAN_POINT ( 'NONE',  ( -83.79436865282308133, 20.08915143297736705, -246.8597181602071373 ) ) ;
#1112=CARTESIAN_POINT ( 'NONE',  ( -221.5672498511017920, 20.79694577634646535, -137.7829567244535269 ) ) ;
#1121=CARTESIAN_POINT ( 'NONE',  ( 59.19439222780464149, 20.08915143297736350, -253.8843055347118138 ) ) ;
#1123=CARTESIAN_POINT ( 'NONE',  ( 159.0697709834164755, 20.79694577659177313, 207.3438552932204857 ) ) ;
#1138=CARTESIAN_POINT ( 'NONE',  ( -130.5770120867059916, 20.08915143302827744, -226.1171533162815024 ) ) ;
#1141=LINE ( 'NONE', #5200, #7870 ) ;
#1160=CARTESIAN_POINT ( 'NONE',  ( 196.2980642835735239, 20.08915143291160632, -172.1812796681614941 ) ) ;
#1161=CARTESIAN_POINT ( 'NONE',  ( 3.196328145774592416E-14, 20.00000000000000000, 261.0000000000000000 ) ) ;
#1169=CARTESIAN_POINT ( 'NONE',  ( 83.86521783953214992, 20.79694577634647601, 247.0684411393755511 ) ) ;
#1171=CARTESIAN_POINT ( 'NONE',  ( 0.000000000000000000, 24.99999999999995737, -246.0000000000000000 ) ) ;
#1180=CARTESIAN_POINT ( 'NONE',  ( -67.47543992451981865, 20.08915143297737060, -251.8100110699624281 ) ) ;
#1190=CARTESIAN_POINT ( 'NONE',  ( 0.000000000000000000, 20.00000000000000000, -261.0000000000000000 ) ) ;
#1194=CARTESIAN_POINT ( 'NONE',  ( -207.3438552936920019, 20.79694577614539597, 159.0697709845790087 ) ) ;
#1198=AXIS2_PLACEMENT_3D ( 'NONE', #7541, #6348, #213 ) ;
#1205=CARTESIAN_POINT ( 'NONE',  ( 17.05314194195614874, 20.08915143307225648, 260.5542428346390125 ) ) ;
#1222=CARTESIAN_POINT ( 'NONE',  ( 17.09264059776268851, 19.96883746064459331, 261.1558126970361400 ) ) ;
#1230=CARTESIAN_POINT ( 'NONE',  ( 212.0849693193239602, 20.79694577634646890, 151.9741924115231484 ) ) ;
#1249=CARTESIAN_POINT ( 'NONE',  ( 34.02434144668549720, 20.08915143297735995, 258.4638482596384392 ) ) ;
#1254=CARTESIAN_POINT ( 'NONE',  ( 259.0935598587374784, 20.79694577687060786, 34.13493237085509691 ) ) ;
#1269=CARTESIAN_POINT ( 'NONE',  ( -226.1171533162824971, 20.08915143300168893, 130.5770120869439950 ) ) ;
#1292=CARTESIAN_POINT ( 'NONE',  ( -130.9697226067400493, 20.55460285172577883, 226.7975291057999527 ) ) ;
#1319=CARTESIAN_POINT ( 'NONE',  ( 221.3800702329289720, 20.08915143297736705, 137.6665579279351732 ) ) ;
#1334=CARTESIAN_POINT ( 'NONE',  ( -247.8175805188620018, 19.96883746128897386, -84.14846197934974725 ) ) ;
#1358=CARTESIAN_POINT ( 'NONE',  ( -247.9906035367588402, 20.55460285060343040, -84.20717312374212327 ) ) ;
#1362=CARTESIAN_POINT ( 'NONE',  ( -221.5672498511021900, 20.79694577634646180, 137.7829567244527880 ) ) ;
#1363=EDGE_CURVE ( 'NONE', #4210, #8633, #7270, .T. ) ;
#1365=CARTESIAN_POINT ( 'NONE',  ( 158.8368823490025932, 20.79694577634646890, -206.9952515782967737 ) ) ;
#1386=CARTESIAN_POINT ( 'NONE',  ( 206.8203823583190228, 20.08915143297735995, -158.7026972336033737 ) ) ;
#1403=CARTESIAN_POINT ( 'NONE',  ( 115.7315435905548071, 19.96883745941821786, 234.7354397751816180 ) ) ;
#1408=CARTESIAN_POINT ( 'NONE',  ( -233.8077470125392949, 20.08915143297735995, 115.3046144132251101 ) ) ;
#1421=CARTESIAN_POINT ( 'NONE',  ( -1.008906662707803564E-12, 19.96883746059272724, 261.1558126970361400 ) ) ;
#1425=CARTESIAN_POINT ( 'NONE',  ( -151.9741924115236031, 20.79694577634646180, 212.0849693193235055 ) ) ;
#1427=CARTESIAN_POINT ( 'NONE',  ( 252.0229195836993199, 20.79694577634646535, -67.53249125288874666 ) ) ;
#1439=EDGE_CURVE ( 'NONE', #953, #4809, #1519, .T. ) ;
#1463=CARTESIAN_POINT ( 'NONE',  ( -159.3024069663917146, 19.96883746063718590, -207.6469600136618681 ) ) ;
#1484=CARTESIAN_POINT ( 'NONE',  ( 261.1558126970361400, 19.96883746059272724, 17.09264059808175062 ) ) ;
#1488=CARTESIAN_POINT ( 'NONE',  ( -206.9952515782971716, 20.79694577634646535, 158.8368823490019395 ) ) ;
#1519=CIRCLE ( 'NONE', #3641, 251.5674242726969680 ) ;
#1525=MANIFOLD_SOLID_BREP ( 'NONE', #716 ) ;
#1529=CARTESIAN_POINT ( 'NONE',  ( 34.18476129334108293, 19.96883746037050855, -259.4723857425807978 ) ) ;
#1550=CARTESIAN_POINT ( 'NONE',  ( -260.7745447056980197, 20.79694577654979071, 17.06760680913495065 ) ) ;
#1551=CARTESIAN_POINT ( 'NONE',  ( 6.337788322448691496E-13, 20.79694577634647601, -260.7745447061711275 ) ) ;
#1558=CARTESIAN_POINT ( 'NONE',  ( 137.7829567244533564, 20.79694577634646890, -221.5672498511020194 ) ) ;
#1572=CARTESIAN_POINT ( 'NONE',  ( -130.5770120867059916, 20.08915143302827744, -226.1171533162815024 ) ) ;
#1577=ORIENTED_EDGE ( 'NONE', *, *, #12335, .F. ) ;
#1584=DIRECTION ( 'NONE',  ( -1.000000000000000000, 0.000000000000000000, 0.000000000000000000 ) ) ;
#1598=CARTESIAN_POINT ( 'NONE',  ( -247.8175805190998062, 19.96883746075563693, 84.14846197946620521 ) ) ;
#1602=AXIS2_PLACEMENT_3D ( 'NONE', #6879, #5745, #6947 ) ;
#1616=CARTESIAN_POINT ( 'NONE',  ( -226.3083638767344894, 20.79694577654763421, 130.6873781513949950 ) ) ;
#1624=CARTESIAN_POINT ( 'NONE',  ( 171.8850263962754070, 20.08915143297735995, 196.0019244007918928 ) ) ;
#1630=CARTESIAN_POINT ( 'NONE',  ( -17.05314194221659818, 20.08915143297737416, -260.5542428351129729 ) ) ;
#1656=ORIENTED_EDGE ( 'NONE', *, *, #6531, .F. ) ;
#1658=CARTESIAN_POINT ( 'NONE',  ( -207.7919029851962023, 20.55460285100346596, -159.4136521840017906 ) ) ;
#1681=CARTESIAN_POINT ( 'NONE',  ( -247.4557548097905055, 20.79694577642381859, 84.02568524162670371 ) ) ;
#1693=CARTESIAN_POINT ( 'NONE',  ( 233.8077470125390676, 20.08915143297735995, 115.3046144132253943 ) ) ;
#1700=LINE ( 'NONE', #9958, #3917 ) ;
#1703=VERTEX_POINT ( 'NONE', #3881 ) ;
#1710=CARTESIAN_POINT ( 'NONE',  ( 0.000000000000000000, 21.94174202707280941, 0.000000000000000000 ) ) ;
#1721=DIRECTION ( 'NONE',  ( 0.000000000000000000, 0.000000000000000000, -1.000000000000000000 ) ) ;
#1728=CARTESIAN_POINT ( 'NONE',  ( -252.9796497735838443, 20.55460285104794949, 67.76049180365761515 ) ) ;
#1733=FILL_AREA_STYLE ('',( #5030 ) ) ;
#1749=CARTESIAN_POINT ( 'NONE',  ( 247.9906035362907915, 20.55460285157398914, 84.20717312406510757 ) ) ;
#1768=CARTESIAN_POINT ( 'NONE',  ( -234.1947771728870009, 20.08915143306511553, -115.4648407706533959 ) ) ;
#1773=ORIENTED_EDGE ( 'NONE', *, *, #7779, .T. ) ;
#1786=CARTESIAN_POINT ( 'NONE',  ( -211.9058003148610112, 20.08915143297736705, 151.8458048843639858 ) ) ;
#1789=CARTESIAN_POINT ( 'NONE',  ( 6.337788322448691496E-13, 20.79694577634647601, -260.7745447061711275 ) ) ;
#1798=CARTESIAN_POINT ( 'NONE',  ( -196.8887528224093444, 20.55460285074426707, 172.6991790975775132 ) ) ;
#1815=EDGE_LOOP ( 'NONE', ( #5492, #1887 ) ) ;
#1817=CARTESIAN_POINT ( 'NONE',  ( -252.4341100429120104, 20.79694577648844245, 67.61424743034129392 ) ) ;
#1834=APPLICATION_CONTEXT ( 'automotive_design' ) ;
#1835=CARTESIAN_POINT ( 'NONE',  ( -67.55708173888510260, 20.08915143292433214, 252.2208631666720180 ) ) ;
#1836=AXIS2_PLACEMENT_3D ( 'NONE', #10262, #12, #4937 ) ;
#1847=CARTESIAN_POINT ( 'NONE',  ( 0.000000000000000000, 24.75600756274008063, 0.000000000000000000 ) ) ;
#1853=CARTESIAN_POINT ( 'NONE',  ( -178.3611219674583310, 20.79694577634646535, -190.4297758776780256 ) ) ;
#1862=CARTESIAN_POINT ( 'NONE',  ( 67.76049180280260487, 20.55460285165543155, -252.9796497734500917 ) ) ;
#1887=ORIENTED_EDGE ( 'NONE', *, *, #7545, .T. ) ;
#1896=CARTESIAN_POINT ( 'NONE',  ( 207.1687172321464914, 20.08915143279739013, 158.9353507257995091 ) ) ;
#1909=CARTESIAN_POINT ( 'NONE',  ( -251.0000000000000000, 22.00000000000000000, 0.000000000000000000 ) ) ;
#1917=CARTESIAN_POINT ( 'NONE',  ( -137.7829567244531006, 20.79694577634646535, -221.5672498511021615 ) ) ;
#1922=ADVANCED_FACE ( 'NONE', ( #12539 ), #3404, .F. ) ;
#1926=CARTESIAN_POINT ( 'NONE',  ( 159.4136521835074802, 20.55460285095908191, 207.7919029867859422 ) ) ;
#1943=CARTESIAN_POINT ( 'NONE',  ( 84.02568524182660781, 20.79694577630801078, -247.4557548099990072 ) ) ;
#1960=CARTESIAN_POINT ( 'NONE',  ( -207.6469600131875666, 19.96883746078517774, 159.3024069659174984 ) ) ;
#1991=CARTESIAN_POINT ( 'NONE',  ( 67.61424743001118998, 20.79694577617620155, -252.4341100437179648 ) ) ;
#2006=CARTESIAN_POINT ( 'NONE',  ( 234.1947771728840166, 20.08915143305504714, -115.4648407707930033 ) ) ;
#2011=CARTESIAN_POINT ( 'NONE',  ( 172.3268284089184874, 20.79694577645659948, 196.4640694358555209 ) ) ;
#2025=CARTESIAN_POINT ( 'NONE',  ( 252.2208631679619941, 20.08915143265656766, 67.55708173926319660 ) ) ;
#2031=CARTESIAN_POINT ( 'NONE',  ( 172.0303573358523010, 20.79694577634646180, 196.1676464792607248 ) ) ;
#2039=DIRECTION ( 'NONE',  ( 0.000000000000000000, 0.000000000000000000, 1.000000000000000000 ) ) ;
#2041=CARTESIAN_POINT ( 'NONE',  ( -225.7689075324034320, 20.08915143297737060, -130.3442252640567744 ) ) ;
#2043=CARTESIAN_POINT ( 'NONE',  ( -172.0303573358527274, 20.79694577634646535, 196.1676464792603269 ) ) ;
#2052=CARTESIAN_POINT ( 'NONE',  ( -115.5625104413703923, 20.79694577664888300, 234.3927740973005029 ) ) ;
#2066=CARTESIAN_POINT ( 'NONE',  ( 196.2980642835735239, 20.08915143291160632, -172.1812796681614941 ) ) ;
#2069=CARTESIAN_POINT ( 'NONE',  ( 260.7745447061710138, 20.79694577634646180, 17.06760680878259961 ) ) ;
#2085=CARTESIAN_POINT ( 'NONE',  ( -130.8783844626380812, 19.96883746054828279, -226.6392846538615231 ) ) ;
#2096=ORIENTED_EDGE ( 'NONE', *, *, #1439, .T. ) ;
#2109=EDGE_CURVE ( 'NONE', #12702, #3706, #11300, .T. ) ;
#2116=CARTESIAN_POINT ( 'NONE',  ( 247.4557548102664839, 20.79694577621951979, -84.02568524171830688 ) ) ;
#2132=CARTESIAN_POINT ( 'NONE',  ( -258.8746690723625079, 20.08915143294039396, -34.10614053585524630 ) ) ;
#2138=CARTESIAN_POINT ( 'NONE',  ( 226.3083638770190191, 20.79694577655596888, 130.6873781509345918 ) ) ;
#2152=CARTESIAN_POINT ( 'NONE',  ( -172.5787240286020392, 19.96883746144090210, 196.7513681798772609 ) ) ;
#2160=CARTESIAN_POINT ( 'NONE',  ( 107.6783259591029065, 20.79694577634646535, 237.6585102388686153 ) ) ;
#2164=ORIENTED_EDGE ( 'NONE', *, *, #5806, .F. ) ;
#2172=CARTESIAN_POINT ( 'NONE',  ( -151.8458048843641848, 20.08915143297736705, -211.9058003148608407 ) ) ;
#2185=CARTESIAN_POINT ( 'NONE',  ( -234.3927740973375080, 20.79694577663154575, -115.5625104413860100 ) ) ;
#2197=DIRECTION ( 'NONE',  ( 0.000000000000000000, -1.000000000000000000, 0.000000000000000000 ) ) ;
#2198=CIRCLE ( 'NONE', #10078, 250.3823410207189966 ) ;
#2200=CARTESIAN_POINT ( 'NONE',  ( 34.10614053541959834, 20.08915143339292442, 258.8746690701424882 ) ) ;
#2221=CARTESIAN_POINT ( 'NONE',  ( 252.8031682264634981, 19.96883746174475860, 67.71318189738019555 ) ) ;
#2250=CARTESIAN_POINT ( 'NONE',  ( 221.3800702329289720, 20.08915143297736705, -137.6665579279351732 ) ) ;
#2253=CARTESIAN_POINT ( 'NONE',  ( 196.4640694355999813, 20.79694577639575570, -172.3268284093740021 ) ) ;
#2259=DIRECTION ( 'NONE',  ( 0.000000000000000000, 0.000000000000000000, 1.000000000000000000 ) ) ;
#2261=CARTESIAN_POINT ( 'NONE',  ( 17.05314194221880086, 20.08915143297735284, -260.5542428351129729 ) ) ;
#2265=DIRECTION ( 'NONE',  ( 0.000000000000000000, -1.000000000000000000, 0.000000000000000000 ) ) ;
#2280=CARTESIAN_POINT ( 'NONE',  ( -1.009183486025028462E-12, 20.55460285106647689, 261.3381329044966606 ) ) ;
#2284=ORIENTED_EDGE ( 'NONE', *, *, #11862, .F. ) ;
#2307=CARTESIAN_POINT ( 'NONE',  ( 91.83222442980247990, 20.08915143297736705, -243.9837273761028769 ) ) ;
#2330=CARTESIAN_POINT ( 'NONE',  ( 84.14846197979342435, 19.96883746137058679, -247.8175805188673735 ) ) ;
#2353=CARTESIAN_POINT ( 'NONE',  ( -207.7919029844864269, 20.55460285060714654, 159.4136521835260112 ) ) ;
#2357=CARTESIAN_POINT ( 'NONE',  ( -244.1900186690934902, 20.79694577634646535, -91.90986972409987743 ) ) ;
#2359=ORIENTED_EDGE ( 'NONE', *, *, #8441, .F. ) ;
#2360=CARTESIAN_POINT ( 'NONE',  ( 254.0989678903619051, 20.79694577634646890, -59.24444182677473947 ) ) ;
#2366=STYLED_ITEM ( 'NONE', ( #10905 ), #1525 ) ;
#2380=CARTESIAN_POINT ( 'NONE',  ( 211.9058003148608407, 20.08915143297736705, -151.8458048843642132 ) ) ;
#2395=CARTESIAN_POINT ( 'NONE',  ( -1.009183486025028462E-12, 20.55460285106647689, 261.3381329044966606 ) ) ;
#2406=CARTESIAN_POINT ( 'NONE',  ( 0.000000000000000000, 19.00000000000000000, 0.000000000000000000 ) ) ;
#2407=ADVANCED_FACE ( 'NONE', ( #8462 ), #11533, .T. ) ;
#2414=AXIS2_PLACEMENT_3D ( 'NONE', #4823, #12966, #774 ) ;
#2417=CARTESIAN_POINT ( 'NONE',  ( 207.6469600143036587, 19.96883745899249618, -159.3024069668460072 ) ) ;
#2423=CARTESIAN_POINT ( 'NONE',  ( 130.4544329367270450, 20.79694577634646535, -225.9597979674043984 ) ) ;
#2436=B_SPLINE_CURVE_WITH_KNOTS ( 'NONE', 3,
 ( #1789, #6411, #12912, #4910, #12113, #724, #3773, #11914, #2764, #785, #2968, #8918, #1917, #11984, #6922, #10981, #1853, #8982, #10045, #3910, #6983, #1112, #495, #6183, #1044, #2357, #11630, #10558, #6433, #7118, #5551, #4356, #7177, #4411, #9609, #10236, #5102, #11564, #5168, #2484, #8435, #4544, #7494, #8496, #1362, #8626, #1488, #3034, #9247, #6500, #2043, #12489, #1425, #53, #6112, #3342, #10165, #9544, #6563, #302, #10618, #8562, #5486, #11176, #7421, #7557 ),
 .UNSPECIFIED., .F., .F.,
 ( 4, 2, 2, 2, 2, 2, 2, 2, 2, 2, 2, 2, 2, 2, 2, 2, 2, 2, 2, 2, 2, 2, 2, 2, 2, 2, 2, 2, 2, 2, 2, 2, 4 ),
 ( 0.5000000000000000000, 0.5156250000000000000, 0.5312500000000000000, 0.5468749999999998890, 0.5624999999999998890, 0.5781249999999998890, 0.5937499999999998890, 0.6093749999999998890, 0.6249999999999998890, 0.6406249999999998890, 0.6562499999999998890, 0.6718749999999998890, 0.6874999999999998890, 0.7031249999999998890, 0.7187499999999998890, 0.7343749999999998890, 0.7499999999999998890, 0.7656249999999998890, 0.7812500000000000000, 0.7968750000000000000, 0.8125000000000000000, 0.8281250000000000000, 0.8437500000000000000, 0.8593750000000000000, 0.8750000000000001110, 0.8906250000000001110, 0.9062500000000002220, 0.9218750000000002220, 0.9375000000000002220, 0.9531250000000001110, 0.9687500000000001110, 0.9843750000000000000, 1.000000000000000000 ),
 .UNSPECIFIED. ) ;
#2460=CARTESIAN_POINT ( 'NONE',  ( -115.7315435904061331, 19.96883746069636700, -234.7354397749499810 ) ) ;
#2464=CARTESIAN_POINT ( 'NONE',  ( -7.780566028168587395E-13, 20.08915143297736350, 260.5542428351130866 ) ) ;
#2465=CARTESIAN_POINT ( 'NONE',  ( -59.19439222780491150, 20.08915143297736705, 253.8843055347117001 ) ) ;
#2478=CARTESIAN_POINT ( 'NONE',  ( -67.76049180359858326, 20.55460285124812359, -252.9796497731095997 ) ) ;
#2484=CARTESIAN_POINT ( 'NONE',  ( -247.0684411393756648, 20.79694577634646535, 83.86521783953146780 ) ) ;
#2486=CARTESIAN_POINT ( 'NONE',  ( 257.4287020129720531, 20.79694577634646890, -42.50473797389749109 ) ) ;
#2524=CARTESIAN_POINT ( 'NONE',  ( -261.1558126970361400, 19.96883746064829168, 17.09264059829825300 ) ) ;
#2544=CARTESIAN_POINT ( 'NONE',  ( 84.20717312453921011, 20.55460285117019126, -247.9906035365278001 ) ) ;
#2570=EDGE_CURVE ( 'NONE', #4210, #8008, #879, .T. ) ;
#2585=CARTESIAN_POINT ( 'NONE',  ( 196.7513681799443361, 19.96883746182971464, 172.5787240285351345 ) ) ;
#2600=ADVANCED_FACE ( 'NONE', ( #780, #2755 ), #3903, .F. ) ;
#2605=CARTESIAN_POINT ( 'NONE',  ( 17.10461161519311091, 20.55460285116648933, 261.3381329044966606 ) ) ;
#2613=EDGE_LOOP ( 'NONE', ( #11994, #8541, #5920, #5414 ) ) ;
#2617=CARTESIAN_POINT ( 'NONE',  ( 115.3046144132256785, 20.08915143297736705, -233.8077470125390676 ) ) ;
#2621=CARTESIAN_POINT ( 'NONE',  ( 130.5770120857756069, 20.08915143320244567, -226.1171533158560010 ) ) ;
#2643=ORIENTED_EDGE ( 'NONE', *, *, #2109, .T. ) ;
#2648=CARTESIAN_POINT ( 'NONE',  ( -115.8123742918135832, 20.55460285136280518, 234.8993005745464586 ) ) ;
#2666=CARTESIAN_POINT ( 'NONE',  ( 196.8887528222392973, 20.55460285123310982, 172.6991790951400390 ) ) ;
#2676=CARTESIAN_POINT ( 'NONE',  ( 253.8843055347118138, 20.08915143297736705, 59.19439222780464149 ) ) ;
#2684=EDGE_CURVE ( 'NONE', #8633, #3549, #1097, .T. ) ;
#2707=CARTESIAN_POINT ( 'NONE',  ( 196.8887528222392973, 20.55460285123310982, 172.6991790951400390 ) ) ;
#2727=CARTESIAN_POINT ( 'NONE',  ( -17.06760680800445229, 20.79694577634651509, -260.7745447061710138 ) ) ;
#2743=CARTESIAN_POINT ( 'NONE',  ( -130.5770120874175859, 20.08915143279216764, 226.1171533172259842 ) ) ;
#2755=FACE_OUTER_BOUND ( 'NONE', #11403, .T. ) ;
#2761=CARTESIAN_POINT ( 'NONE',  ( -260.5542428351132571, 20.08915143297737060, -8.526617657838357900 ) ) ;
#2764=CARTESIAN_POINT ( 'NONE',  ( -91.90986972409933742, 20.79694577634647246, -244.1900186690937460 ) ) ;
#2774=CARTESIAN_POINT ( 'NONE',  ( 234.8993005733554185, 20.55460285121469610, -115.8123742911327838 ) ) ;
#2788=CARTESIAN_POINT ( 'NONE',  ( 130.5770120874479971, 20.08915143273683412, 226.1171533175384809 ) ) ;
#2796=CARTESIAN_POINT ( 'NONE',  ( -207.3438552936920019, 20.79694577614539597, 159.0697709845790087 ) ) ;
#2816=SHAPE_REPRESENTATION_RELATIONSHIP ( 'NONE' , 'NONE' ,  #8443, #11752 ) ;
#2839=TOROIDAL_SURFACE ( 'NONE', #7968, 250.3823410207189966, 3.000000000000000000 ) ;
#2843=CARTESIAN_POINT ( 'NONE',  ( -247.9906035374705766, 20.55460285117394648, 84.20717312385856701 ) ) ;
#2864=CARTESIAN_POINT ( 'NONE',  ( 234.3927740981229988, 20.79694577626769103, 115.5625104417014057 ) ) ;
#2882=CARTESIAN_POINT ( 'NONE',  ( 158.9353507248500250, 20.08915143321791419, 207.1687172302519855 ) ) ;
#2888=VERTEX_POINT ( 'NONE', #9498 ) ;
#2902=EDGE_LOOP ( 'NONE', ( #1577, #1656, #5673, #12493 ) ) ;
#2906=CARTESIAN_POINT ( 'NONE',  ( -115.8123742913374770, 20.55460285152583921, -234.8993005728878529 ) ) ;
#2926=B_SPLINE_CURVE_WITH_KNOTS ( 'NONE', 3,
 ( #12977, #9590, #475, #9977, #8607, #2465, #8980, #4522, #6479, #12666, #6542, #4832, #4457, #5782, #3839, #12790, #7981, #5466, #8848, #9527, #1786, #10536, #9841, #1408, #11674, #9911, #3528, #7596, #12909, #3770, #406, #7840, #8542, #2761, #12601, #5853, #3459, #7537, #8915, #11610, #10162, #10302, #4104, #2041, #1041, #3031, #179, #8115, #12174, #9308, #12246, #7174, #2172, #4237, #6250, #7046, #6427, #4172, #1110, #1180, #9106, #8251, #12109, #12307, #3162, #51 ),
 .UNSPECIFIED., .F., .F.,
 ( 4, 2, 2, 2, 2, 2, 2, 2, 2, 2, 2, 2, 2, 2, 2, 2, 2, 2, 2, 2, 2, 2, 2, 2, 2, 2, 2, 2, 2, 2, 2, 2, 4 ),
 ( 0.000000000000000000, 0.01562500000000000347, 0.03125000000000001388, 0.04687500000000002776, 0.06250000000000001388, 0.07812500000000000000, 0.09374999999999998612, 0.1093749999999999861, 0.1249999999999999722, 0.1406249999999999722, 0.1562499999999999722, 0.1718749999999999722, 0.1874999999999999722, 0.2031250000000000000, 0.2187500000000000000, 0.2343750000000000000, 0.2500000000000000000, 0.2656250000000000000, 0.2812500000000000000, 0.2968750000000000000, 0.3125000000000000000, 0.3281250000000000000, 0.3437500000000000000, 0.3593750000000000000, 0.3750000000000000000, 0.3906250000000000555, 0.4062500000000000555, 0.4218750000000000555, 0.4375000000000000555, 0.4531250000000000555, 0.4687500000000000555, 0.4843750000000000555, 0.5000000000000000000 ),
 .UNSPECIFIED. ) ;
#2943=APPLICATION_CONTEXT ( 'automotive_design' ) ;
#2949=CARTESIAN_POINT ( 'NONE',  ( 226.1171533175249806, 20.08915143274010262, -130.5770120874387885 ) ) ;
#2950=DIRECTION ( 'NONE',  ( 0.000000000000000000, -1.000000000000000000, 0.000000000000000000 ) ) ;
#2954=DIRECTION ( 'NONE',  ( 0.000000000000000000, 1.000000000000000000, 0.000000000000000000 ) ) ;
#2968=CARTESIAN_POINT ( 'NONE',  ( -115.4021059068215180, 20.79694577634647246, -234.0054343868620492 ) ) ;
#2978=CARTESIAN_POINT ( 'NONE',  ( -252.4341100429099924, 20.79694577648418985, -67.61424743040240060 ) ) ;
#2993=FACE_OUTER_BOUND ( 'NONE', #3241, .T. ) ;
#3012=CARTESIAN_POINT ( 'NONE',  ( -196.7513681801157759, 19.96883745974439961, 172.5787240288376836 ) ) ;
#3013=FACE_OUTER_BOUND ( 'NONE', #7896, .T. ) ;
#3031=CARTESIAN_POINT ( 'NONE',  ( -211.9058003148605280, 20.08915143297737060, -151.8458048843646964 ) ) ;
#3034=CARTESIAN_POINT ( 'NONE',  ( -196.1676464792609806, 20.79694577634646535, 172.0303573358519316 ) ) ;
#3045=CARTESIAN_POINT ( 'NONE',  ( -130.6873781523279945, 20.79694577633451402, 226.3083638767075172 ) ) ;
#3061=CARTESIAN_POINT ( 'NONE',  ( 34.10614053577565130, 20.08915143319461905, -258.8746690710824510 ) ) ;
#3067=CARTESIAN_POINT ( 'NONE',  ( 130.6873781507030117, 20.79694577677803125, -226.3083638765525052 ) ) ;
#3068=CARTESIAN_POINT ( 'NONE',  ( 0.000000000000000000, 20.00000000000000000, 0.000000000000000000 ) ) ;
#3075=DIRECTION ( 'NONE',  ( 0.000000000000000000, -1.000000000000000000, 0.000000000000000000 ) ) ;
#3076=ORIENTED_EDGE ( 'NONE', *, *, #4669, .F. ) ;
#3078=CARTESIAN_POINT ( 'NONE',  ( 0.000000000000000000, 21.99999999999995381, 0.000000000000000000 ) ) ;
#3081=CARTESIAN_POINT ( 'NONE',  ( -252.8031682270700458, 19.96883746027420869, -67.71318189758747508 ) ) ;
#3088=CARTESIAN_POINT ( 'NONE',  ( 260.3553053170167004, 20.79694577634646890, 17.06764083276451771 ) ) ;
#3104=ORIENTED_EDGE ( 'NONE', *, *, #12408, .F. ) ;
#3109=EDGE_LOOP ( 'NONE', ( #2096, #6900, #1773, #4977 ) ) ;
#3110=CARTESIAN_POINT ( 'NONE',  ( 207.3438552925264844, 20.79694577678052880, -159.0697709836649949 ) ) ;
#3122=CARTESIAN_POINT ( 'NONE',  ( 115.4648407705614090, 20.08915143315789109, 234.1947771724234713 ) ) ;
#3143=CARTESIAN_POINT ( 'NONE',  ( -234.7354397751870749, 19.96883746042966123, 115.7315435905245522 ) ) ;
#3162=CARTESIAN_POINT ( 'NONE',  ( -8.526617657837745057, 20.08915143297736705, -260.5542428351132571 ) ) ;
#3166=ORIENTED_EDGE ( 'NONE', *, *, #7779, .F. ) ;
#3176=CARTESIAN_POINT ( 'NONE',  ( -84.02568524195829980, 20.79694577620390916, -247.4557548102065141 ) ) ;
#3188=CARTESIAN_POINT ( 'NONE',  ( 67.55708173896789503, 20.08915143276009729, -252.2208631674930359 ) ) ;
#3210=CARTESIAN_POINT ( 'NONE',  ( 261.1558126970361400, 19.96883746059272724, -17.09264059807959057 ) ) ;
#3224=CONICAL_SURFACE ( 'NONE', #10682, 251.0000000000000000, 1.164698268477292631 ) ;
#3241=EDGE_LOOP ( 'NONE', ( #307, #8037, #7759, #6714 ) ) ;
#3242=CARTESIAN_POINT ( 'NONE',  ( -130.6873781513712061, 20.79694577639645203, -226.3083638771730079 ) ) ;
#3256=CARTESIAN_POINT ( 'NONE',  ( 258.8746690706134927, 20.08915143329815933, 34.10614053548034974 ) ) ;
#3276=CARTESIAN_POINT ( 'NONE',  ( 234.7354397751814759, 19.96883746015188876, -115.7315435904363312 ) ) ;
#3281=CARTESIAN_POINT ( 'NONE',  ( 17.06764083276447153, 20.79694577634646890, 260.3553053170167004 ) ) ;
#3298=ORIENTED_EDGE ( 'NONE', *, *, #7545, .F. ) ;
#3306=CARTESIAN_POINT ( 'NONE',  ( 83.79436865282355029, 20.08915143297736705, 246.8597181602068815 ) ) ;
#3320=CARTESIAN_POINT ( 'NONE',  ( 207.1687172321464914, 20.08915143279739013, 158.9353507257995091 ) ) ;
#3338=CARTESIAN_POINT ( 'NONE',  ( 247.8175805195787689, 19.96883746176681740, 84.14846197955617413 ) ) ;
#3342=CARTESIAN_POINT ( 'NONE',  ( -115.4021059068222570, 20.79694577634646535, 234.0054343868616797 ) ) ;
#3344=CARTESIAN_POINT ( 'NONE',  ( 190.4297758776777982, 20.79694577634646180, 178.3611219674585584 ) ) ;
#3357=CIRCLE ( 'NONE', #12524, 246.0000000000000000 ) ;
#3365=CARTESIAN_POINT ( 'NONE',  ( 107.5873595010540384, 20.08915143297736350, -237.4577367525705256 ) ) ;
#3385=CARTESIAN_POINT ( 'NONE',  ( 130.8783844624215931, 19.96883746229290679, 226.6392846534563716 ) ) ;
#3392=CYLINDRICAL_SURFACE ( 'NONE', #11345, 246.0000000000000000 ) ;
#3404=TOROIDAL_SURFACE ( 'NONE', #7887, 250.7029414592220178, 3.000000000000000000 ) ;
#3405=CARTESIAN_POINT ( 'NONE',  ( -159.4136521839998011, 20.55460285116278385, -207.7919029849606432 ) ) ;
#3430=ORIENTED_EDGE ( 'NONE', *, *, #5424, .T. ) ;
#3433=CARTESIAN_POINT ( 'NONE',  ( 3.073828142905996055E-14, 22.00000000000000000, -250.7029414592220178 ) ) ;
#3435=CARTESIAN_POINT ( 'NONE',  ( 246.8597181602069384, 20.08915143297736350, 83.79436865282337976 ) ) ;
#3453=CARTESIAN_POINT ( 'NONE',  ( -259.4723857429225404, 19.96883746178179209, 34.18476129330913693 ) ) ;
#3459=CARTESIAN_POINT ( 'NONE',  ( -257.2112267038639288, 20.08915143297736705, -42.46883004693722796 ) ) ;
#3478=CARTESIAN_POINT ( 'NONE',  ( 247.8175805191053769, 19.96883746103348045, -84.14846197955421303 ) ) ;
#3483=VERTEX_POINT ( 'NONE', #11386 ) ;
#3516=EDGE_CURVE ( 'NONE', #8008, #2888, #11318, .T. ) ;
#3523=CARTESIAN_POINT ( 'NONE',  ( -259.4723857429215741, 19.96883746091132394, -34.18476129331127567 ) ) ;
#3527=CONICAL_SURFACE ( 'NONE', #1836, 251.0000000000000000, 1.164698268477292631 ) ;
#3528=CARTESIAN_POINT ( 'NONE',  ( -246.8597181602071657, 20.08915143297736705, 83.79436865282285396 ) ) ;
#3540=CARTESIAN_POINT ( 'NONE',  ( 207.7919029844146053, 20.55460285114793351, 159.4136521835094413 ) ) ;
#3544=DIRECTION ( 'NONE',  ( 0.000000000000000000, 0.000000000000000000, -1.000000000000000000 ) ) ;
#3548=CARTESIAN_POINT ( 'NONE',  ( 196.1676464792607248, 20.79694577634646890, -172.0303573358522726 ) ) ;
#3549=VERTEX_POINT ( 'NONE', #3433 ) ;
#3562=EDGE_LOOP ( 'NONE', ( #8213, #11924, #3430, #2359 ) ) ;
#3583=CARTESIAN_POINT ( 'NONE',  ( 0.000000000000000000, 24.99999999999995737, -251.0000000000000000 ) ) ;
#3587=CARTESIAN_POINT ( 'NONE',  ( 172.5787240287722284, 19.96883746003332405, -196.7513681799441656 ) ) ;
#3608=CARTESIAN_POINT ( 'NONE',  ( 247.9906035370026984, 20.55460285091836070, -84.20717312441868785 ) ) ;
#3615=CARTESIAN_POINT ( 'NONE',  ( 234.0054343868619355, 20.79694577634646890, -115.4021059068217738 ) ) ;
#3641=AXIS2_PLACEMENT_3D ( 'NONE', #1847, #11034, #5910 ) ;
#3650=CARTESIAN_POINT ( 'NONE',  ( -234.7354397751870749, 19.96883746042966123, 115.7315435905245522 ) ) ;
#3674=CARTESIAN_POINT ( 'NONE',  ( -115.5625104413703923, 20.79694577664888300, 234.3927740973005029 ) ) ;
#3687=CARTESIAN_POINT ( 'NONE',  ( 158.7026972336034021, 20.08915143297736705, 206.8203823583190797 ) ) ;
#3706=VERTEX_POINT ( 'NONE', #1171 ) ;
#3723=CARTESIAN_POINT ( 'NONE',  ( 247.9906035362907915, 20.55460285157398914, 84.20717312406510757 ) ) ;
#3739=CARTESIAN_POINT ( 'NONE',  ( -1.009475258464312158E-12, 20.08915143297736350, 260.5542428351129729 ) ) ;
#3741=CARTESIAN_POINT ( 'NONE',  ( -67.61424743045878927, 20.79694577628127661, -252.4341100433800023 ) ) ;
#3770=CARTESIAN_POINT ( 'NONE',  ( -257.2112267038639288, 20.08915143297736705, 42.46883004693641084 ) ) ;
#3773=CARTESIAN_POINT ( 'NONE',  ( -67.53249125288850507, 20.79694577634646890, -252.0229195836992631 ) ) ;
#3782=CARTESIAN_POINT ( 'NONE',  ( -17.10461161402953323, 20.55460285106647689, -261.3381329044966606 ) ) ;
#3807=CARTESIAN_POINT ( 'NONE',  ( -252.4341100429099924, 20.79694577648418985, -67.61424743040240060 ) ) ;
#3824=CARTESIAN_POINT ( 'NONE',  ( -34.10614053579494964, 20.08915143303473982, -258.8746690718934929 ) ) ;
#3839=CARTESIAN_POINT ( 'NONE',  ( -158.7026972336038284, 20.08915143297736705, 206.8203823583187386 ) ) ;
#3852=CARTESIAN_POINT ( 'NONE',  ( 247.9906035370026984, 20.55460285091836070, -84.20717312441868785 ) ) ;
#3873=CARTESIAN_POINT ( 'NONE',  ( 115.5625104413773983, 20.79694577638496966, -234.3927740979615066 ) ) ;
#3881=CARTESIAN_POINT ( 'NONE',  ( 3.073555866996735681E-14, 24.99999999999995737, 250.3823410207189966 ) ) ;
#3891=CARTESIAN_POINT ( 'NONE',  ( -34.10614053585819505, 20.08915143303038775, 258.8746690719034973 ) ) ;
#3903=PLANE ( 'NONE',  #12797 ) ;
#3910=CARTESIAN_POINT ( 'NONE',  ( -206.9952515782967168, 20.79694577634646535, -158.8368823490026500 ) ) ;
#3917=VECTOR ( 'NONE', #12828, 1000.000000000000000 ) ;
#3921=CARTESIAN_POINT ( 'NONE',  ( -67.76049180359858326, 20.55460285124812359, -252.9796497731095997 ) ) ;
#3937=DIRECTION ( 'NONE',  ( 0.000000000000000000, 1.000000000000000000, 0.000000000000000000 ) ) ;
#3939=CARTESIAN_POINT ( 'NONE',  ( 252.4341100445949735, 20.79694577582237613, 67.61424742981928659 ) ) ;
#3956=CARTESIAN_POINT ( 'NONE',  ( -34.18476129408180242, 19.96883745937779864, 259.4723857443443080 ) ) ;
#3973=UNCERTAINTY_MEASURE_WITH_UNIT (LENGTH_MEASURE( 1.000000000000000082E-05 ), #8905, 'distance_accuracy_value', 'NONE');
#3980=CARTESIAN_POINT ( 'NONE',  ( -247.4557548106230058, 20.79694577606145600, -84.02568524181840814 ) ) ;
#4020=CARTESIAN_POINT ( 'NONE',  ( -1.009475258464312158E-12, 20.08915143297736350, 260.5542428351129729 ) ) ;
#4051=CARTESIAN_POINT ( 'NONE',  ( 260.7745447061710138, 20.79694577634651509, -17.06760680878044667 ) ) ;
#4065=MECHANICAL_DESIGN_GEOMETRIC_PRESENTATION_REPRESENTATION('',(#2366),#6382);
#4067=CARTESIAN_POINT ( 'NONE',  ( -234.1947771733725006, 20.08915143296620442, 115.4648407707744013 ) ) ;
#4085=ORIENTED_EDGE ( 'NONE', *, *, #11847, .F. ) ;
#4087=CARTESIAN_POINT ( 'NONE',  ( -259.4723857429215741, 19.96883746091132394, -34.18476129331127567 ) ) ;
#4093=CARTESIAN_POINT ( 'NONE',  ( 257.4287020129719963, 20.79694577634646535, 42.50473797389774688 ) ) ;
#4104=CARTESIAN_POINT ( 'NONE',  ( -233.8077470125389254, 20.08915143297736705, -115.3046144132258917 ) ) ;
#4112=FACE_BOUND ( 'NONE', #11713, .T. ) ;
#4120=CARTESIAN_POINT ( 'NONE',  ( -159.0697709836499882, 20.79694577635847352, 207.3438552937170130 ) ) ;
#4134=CARTESIAN_POINT ( 'NONE',  ( -207.1687172315079692, 20.08915143295307004, 158.9353507253535156 ) ) ;
#4147=CARTESIAN_POINT ( 'NONE',  ( 0.000000000000000000, 21.94174202707280941, 251.2912898646363828 ) ) ;
#4152=CARTESIAN_POINT ( 'NONE',  ( 260.5542428351129729, 20.08915143297735284, 17.05314194231024771 ) ) ;
#4172=CARTESIAN_POINT ( 'NONE',  ( -91.83222442980213884, 20.08915143297737060, -243.9837273761029621 ) ) ;
#4179=CARTESIAN_POINT ( 'NONE',  ( 83.79436865282340818, 20.08915143297736705, -246.8597181602070805 ) ) ;
#4182=CARTESIAN_POINT ( 'NONE',  ( 34.13493236988740165, 20.79694577678859702, 259.0935598591244684 ) ) ;
#4195=CARTESIAN_POINT ( 'NONE',  ( -158.9353507255915190, 20.08915143292644245, -207.1687172315094756 ) ) ;
#4210=VERTEX_POINT ( 'NONE', #4147 ) ;
#4215=CARTESIAN_POINT ( 'NONE',  ( 67.76049180280260487, 20.55460285165543155, -252.9796497734500917 ) ) ;
#4222=CARTESIAN_POINT ( 'NONE',  ( 178.3611219674583310, 20.79694577634646535, 190.4297758776779403 ) ) ;
#4237=CARTESIAN_POINT ( 'NONE',  ( -137.6665579279351448, 20.08915143297737060, -221.3800702329289720 ) ) ;
#4250=CARTESIAN_POINT ( 'NONE',  ( -67.61424743051179576, 20.79694577629433283, 252.4341100433384781 ) ) ;
#4262=CARTESIAN_POINT ( 'NONE',  ( -67.71318189681706201, 19.96883746180772690, 252.8031682256479655 ) ) ;
#4280=ADVANCED_FACE ( 'NONE', ( #9216 ), #220, .F. ) ;
#4283=CARTESIAN_POINT ( 'NONE',  ( -226.7975291067479588, 20.55460285112940610, -130.9697226053176564 ) ) ;
#4285=CARTESIAN_POINT ( 'NONE',  ( 84.02568524192950861, 20.79694577611522632, 247.4557548104415048 ) ) ;
#4327=CARTESIAN_POINT ( 'NONE',  ( 130.5770120874479971, 20.08915143273683412, 226.1171533175384809 ) ) ;
#4352=CARTESIAN_POINT ( 'NONE',  ( 252.8031682264636117, 19.96883746172993668, -67.71318189737802129 ) ) ;
#4356=CARTESIAN_POINT ( 'NONE',  ( -260.3553053170167004, 20.79694577634646535, -17.06764083276478772 ) ) ;
#4359=CARTESIAN_POINT ( 'NONE',  ( 252.0229195836992062, 20.79694577634646535, 67.53249125288881771 ) ) ;
#4379=CARTESIAN_POINT ( 'NONE',  ( 137.6665579279354006, 20.08915143297737060, -221.3800702329289152 ) ) ;
#4389=CARTESIAN_POINT ( 'NONE',  ( 172.5787240287708073, 19.96883745935533838, 196.7513681801829932 ) ) ;
#4393=EDGE_CURVE ( 'NONE', #2888, #8825, #12867, .T. ) ;
#4400=CARTESIAN_POINT ( 'NONE',  ( 6.337788322448691496E-13, 20.79694577634647601, -260.7745447061711275 ) ) ;
#4406=CARTESIAN_POINT ( 'NONE',  ( -172.6991790971032970, 20.55460285072942384, -196.8887528238318509 ) ) ;
#4411=CARTESIAN_POINT ( 'NONE',  ( -260.7745447061711843, 20.79694577634646535, 8.533827019709271156 ) ) ;
#4413=CARTESIAN_POINT ( 'NONE',  ( 34.05310945291996916, 20.79694577634646535, -258.6823826759385270 ) ) ;
#4436=CARTESIAN_POINT ( 'NONE',  ( 251.8100110699623144, 20.08915143297736705, -67.47543992452008865 ) ) ;
#4452=CARTESIAN_POINT ( 'NONE',  ( -234.7354397754233446, 19.96883745989621417, -115.7315435906453871 ) ) ;
#4457=CARTESIAN_POINT ( 'NONE',  ( -137.6665579279357701, 20.08915143297736705, 221.3800702329286310 ) ) ;
#4472=CARTESIAN_POINT ( 'NONE',  ( -34.20858920445061102, 20.55460285115536934, 259.6535381498995321 ) ) ;
#4478=ORIENTED_EDGE ( 'NONE', *, *, #2570, .T. ) ;
#4516=CARTESIAN_POINT ( 'NONE',  ( -252.8031682270700458, 19.96883746027420869, -67.71318189758747508 ) ) ;
#4522=CARTESIAN_POINT ( 'NONE',  ( -83.79436865282377767, 20.08915143297736705, 246.8597181602068531 ) ) ;
#4539=CARTESIAN_POINT ( 'NONE',  ( -196.4640694352650030, 20.79694577634417030, 172.3268284098779759 ) ) ;
#4544=CARTESIAN_POINT ( 'NONE',  ( -237.6585102388689563, 20.79694577634646535, 107.6783259591022244 ) ) ;
#4546=CARTESIAN_POINT ( 'NONE',  ( 244.1900186690937460, 20.79694577634646535, -91.90986972409935163 ) ) ;
#4551=ORIENTED_EDGE ( 'NONE', *, *, #5016, .T. ) ;
#4582=ORIENTED_EDGE ( 'NONE', *, *, #10724, .F. ) ;
#4584=CARTESIAN_POINT ( 'NONE',  ( 196.7513681799458709, 19.96883746115198122, -172.5787240287706936 ) ) ;
#4601=CARTESIAN_POINT ( 'NONE',  ( 261.3381329044966606, 20.55460285106647689, -17.10461161501038063 ) ) ;
#4608=CARTESIAN_POINT ( 'NONE',  ( 237.6585102388688426, 20.79694577634646890, -107.6783259591024802 ) ) ;
#4616=CARTESIAN_POINT ( 'NONE',  ( 34.10614053577565130, 20.08915143319461905, -258.8746690710824510 ) ) ;
#4627=DIRECTION ( 'NONE',  ( 1.000000000000000000, 0.000000000000000000, 0.000000000000000000 ) ) ;
#4645=CARTESIAN_POINT ( 'NONE',  ( -207.6469600131875666, 19.96883746078517774, 159.3024069659174984 ) ) ;
#4668=CARTESIAN_POINT ( 'NONE',  ( -259.0935598604229995, 20.79694577620878704, -34.13493237027169158 ) ) ;
#4669=EDGE_CURVE ( 'NONE', #4809, #953, #9425, .T. ) ;
#4680=CARTESIAN_POINT ( 'NONE',  ( 225.7689075324037162, 20.08915143297736705, -130.3442252640562913 ) ) ;
#4693=DIRECTION ( 'NONE',  ( 0.000000000000000000, 0.000000000000000000, -1.000000000000000000 ) ) ;
#4712=CARTESIAN_POINT ( 'NONE',  ( -130.9697226067400493, 20.55460285172577883, 226.7975291057999527 ) ) ;
#4733=FACE_OUTER_BOUND ( 'NONE', #821, .T. ) ;
#4736=CARTESIAN_POINT ( 'NONE',  ( 159.4136521835074802, 20.55460285095908191, 207.7919029867859422 ) ) ;
#4749=CARTESIAN_POINT ( 'NONE',  ( 59.19439222780480492, 20.08915143297736705, 253.8843055347117001 ) ) ;
#4754=CARTESIAN_POINT ( 'NONE',  ( -196.2980642832790181, 20.08915143307791951, 172.1812796672794832 ) ) ;
#4784=CARTESIAN_POINT ( 'NONE',  ( 207.7919029844146053, 20.55460285114793351, 159.4136521835094413 ) ) ;
#4804=CARTESIAN_POINT ( 'NONE',  ( 67.76049180374880621, 20.55460285150727273, 252.9796497720274147 ) ) ;
#4809=VERTEX_POINT ( 'NONE', #10655 ) ;
#4817=CARTESIAN_POINT ( 'NONE',  ( -234.1947771733725006, 20.08915143296620442, 115.4648407707744013 ) ) ;
#4823=CARTESIAN_POINT ( 'NONE',  ( 0.000000000000000000, 21.94174202707280941, 0.000000000000000000 ) ) ;
#4829=SURFACE_STYLE_USAGE ( .BOTH. , #48 ) ;
#4832=CARTESIAN_POINT ( 'NONE',  ( -130.3442252640568029, 20.08915143297736705, 225.7689075324034036 ) ) ;
#4845=EDGE_CURVE ( 'NONE', #953, #8825, #10463, .T. ) ;
#4850=CARTESIAN_POINT ( 'NONE',  ( 259.6535381495593242, 20.55460285082940075, -34.20858920423904692 ) ) ;
#4873=CARTESIAN_POINT ( 'NONE',  ( 34.13493236988740165, 20.79694577678859702, 259.0935598591244684 ) ) ;
#4891=CARTESIAN_POINT ( 'NONE',  ( -1.009475258464312158E-12, 20.08915143297736350, 260.5542428351129729 ) ) ;
#4910=CARTESIAN_POINT ( 'NONE',  ( -34.05310945291963520, 20.79694577634646180, -258.6823826759385270 ) ) ;
#4919=CARTESIAN_POINT ( 'NONE',  ( 17.10461161403171815, 20.55460285106647689, -261.3381329044966606 ) ) ;
#4935=CARTESIAN_POINT ( 'NONE',  ( -34.10614053585819505, 20.08915143303038775, 258.8746690719034973 ) ) ;
#4937=DIRECTION ( 'NONE',  ( 0.000000000000000000, 0.000000000000000000, -1.000000000000000000 ) ) ;
#4955=CARTESIAN_POINT ( 'NONE',  ( 115.7315435902013263, 19.96883745981483926, -234.7354397754176318 ) ) ;
#4977=ORIENTED_EDGE ( 'NONE', *, *, #4845, .F. ) ;
#4984=CARTESIAN_POINT ( 'NONE',  ( 34.20858920406338655, 20.55460285047751157, -259.6535381481361355 ) ) ;
#5001=CARTESIAN_POINT ( 'NONE',  ( 0.000000000000000000, 21.99999999999995381, -250.3823410207189966 ) ) ;
#5003=CARTESIAN_POINT ( 'NONE',  ( 0.000000000000000000, 19.00000000000000000, 0.000000000000000000 ) ) ;
#5005=FACE_OUTER_BOUND ( 'NONE', #11902, .T. ) ;
#5016=EDGE_CURVE ( 'NONE', #2888, #6668, #834, .T. ) ;
#5020=CARTESIAN_POINT ( 'NONE',  ( 234.1947771726669885, 20.08915143309429041, 115.4648407708036046 ) ) ;
#5022=( NAMED_UNIT ( * ) SI_UNIT ( $, .STERADIAN. ) SOLID_ANGLE_UNIT ( ) );
#5030=FILL_AREA_STYLE_COLOUR ( '', #13014 ) ;
#5043=CARTESIAN_POINT ( 'NONE',  ( 207.3438552934050279, 20.79694577613707551, 159.0697709850429931 ) ) ;
#5059=CARTESIAN_POINT ( 'NONE',  ( -247.2466869557850089, 20.08915143288961858, -83.95474316020511196 ) ) ;
#5064=CARTESIAN_POINT ( 'NONE',  ( 259.0935598587374784, 20.79694577687060786, 34.13493237085509691 ) ) ;
#5082=CARTESIAN_POINT ( 'NONE',  ( -259.4723857429225404, 19.96883746178179209, 34.18476129330913693 ) ) ;
#5092=ORIENTED_EDGE ( 'NONE', *, *, #5835, .T. ) ;
#5100=DIRECTION ( 'NONE',  ( 1.000000000000000000, 0.000000000000000000, -1.224646799147353207E-16 ) ) ;
#5102=CARTESIAN_POINT ( 'NONE',  ( -257.4287020129719963, 20.79694577634646180, 42.50473797389691555 ) ) ;
#5113=CARTESIAN_POINT ( 'NONE',  ( -247.4557548097905055, 20.79694577642381859, 84.02568524162670371 ) ) ;
#5126=CARTESIAN_POINT ( 'NONE',  ( 130.5770120857756069, 20.08915143320244567, -226.1171533158560010 ) ) ;
#5132=CARTESIAN_POINT ( 'NONE',  ( 159.0697709852749995, 20.79694577591498472, -207.3438552938715134 ) ) ;
#5147=CARTESIAN_POINT ( 'NONE',  ( -17.09264059789343193, 19.96883746059643983, -261.1558126970361400 ) ) ;
#5153=CARTESIAN_POINT ( 'NONE',  ( 137.7829567244532143, 20.79694577634646180, 221.5672498511019626 ) ) ;
#5158=ORIENTED_EDGE ( 'NONE', *, *, #1439, .F. ) ;
#5159=VECTOR ( 'NONE', #10555, 1000.000000000000000 ) ;
#5168=CARTESIAN_POINT ( 'NONE',  ( -252.0229195836994336, 20.79694577634646535, 67.53249125288826349 ) ) ;
#5177=ORIENTED_EDGE ( 'NONE', *, *, #4393, .T. ) ;
#5180=CARTESIAN_POINT ( 'NONE',  ( -196.4640694359484883, 20.79694577636040265, -172.3268284091419957 ) ) ;
#5196=CARTESIAN_POINT ( 'NONE',  ( -226.1171533167550081, 20.08915143289658545, -130.5770120871825952 ) ) ;
#5200=CARTESIAN_POINT ( 'NONE',  ( 3.012631125902489062E-14, 23.50000000000000000, 246.0000000000000000 ) ) ;
#5217=CARTESIAN_POINT ( 'NONE',  ( 207.1687172302655142, 20.08915143321463503, -158.9353507248590063 ) ) ;
#5237=DIRECTION ( 'NONE',  ( 0.000000000000000000, -1.000000000000000000, 0.000000000000000000 ) ) ;
#5245=DIRECTION ( 'NONE',  ( 0.000000000000000000, -0.1961161351381850160, -0.9805806756909200006 ) ) ;
#5250=CARTESIAN_POINT ( 'NONE',  ( -260.7745447066434963, 20.79694577614318618, -17.06760680913714978 ) ) ;
#5264=CARTESIAN_POINT ( 'NONE',  ( -1.009475258464312158E-12, 20.08915143297736350, 260.5542428351129729 ) ) ;
#5283=CARTESIAN_POINT ( 'NONE',  ( 172.5787240287722284, 19.96883746003332405, -196.7513681799441656 ) ) ;
#5284=CARTESIAN_POINT ( 'NONE',  ( 0.000000000000000000, 22.00000000000000000, 250.7029414592220178 ) ) ;
#5290=CARTESIAN_POINT ( 'NONE',  ( 115.4021059068215607, 20.79694577634647246, 234.0054343868620208 ) ) ;
#5319=CARTESIAN_POINT ( 'NONE',  ( 196.4640694362159934, 20.79694577623644491, 172.3268284092819727 ) ) ;
#5332=CARTESIAN_POINT ( 'NONE',  ( 247.2466869560049929, 20.08915143286045790, 83.95474316005440585 ) ) ;
#5356=CARTESIAN_POINT ( 'NONE',  ( 159.3024069666089133, 19.96883745889249795, 207.6469600140662806 ) ) ;
#5362=CARTESIAN_POINT ( 'NONE',  ( 67.53249125288894561, 20.79694577634646180, 252.0229195836991494 ) ) ;
#5383=DIRECTION ( 'NONE',  ( 0.000000000000000000, -1.000000000000000000, 0.000000000000000000 ) ) ;
#5386=CARTESIAN_POINT ( 'NONE',  ( 171.8850263962756628, 20.08915143297737416, -196.0019244007918644 ) ) ;
#5401=CARTESIAN_POINT ( 'NONE',  ( 252.8031682264636117, 19.96883746172993668, -67.71318189737802129 ) ) ;
#5414=ORIENTED_EDGE ( 'NONE', *, *, #1363, .F. ) ;
#5423=CARTESIAN_POINT ( 'NONE',  ( 115.7315435905548071, 19.96883745941821786, 234.7354397751816180 ) ) ;
#5424=EDGE_CURVE ( 'NONE', #9039, #10670, #3357, .T. ) ;
#5448=CARTESIAN_POINT ( 'NONE',  ( 0.000000000000000000, 24.99999999999995737, 0.000000000000000000 ) ) ;
#5449=CARTESIAN_POINT ( 'NONE',  ( 246.8597181602070521, 20.08915143297736705, -83.79436865282332292 ) ) ;
#5462=CARTESIAN_POINT ( 'NONE',  ( -17.10461161519512174, 20.55460285096646089, 261.3381329044966606 ) ) ;
#5466=CARTESIAN_POINT ( 'NONE',  ( -190.2689011420773966, 20.08915143297736705, 178.2104428091925001 ) ) ;
#5469=FACE_OUTER_BOUND ( 'NONE', #2902, .T. ) ;
#5474=CARTESIAN_POINT ( 'NONE',  ( 6.345753394971347358E-13, 20.08915143297736350, -260.5542428351130866 ) ) ;
#5480=CARTESIAN_POINT ( 'NONE',  ( -84.20717312421410838, 20.55460285060721048, -247.9906035374705766 ) ) ;
#5486=CARTESIAN_POINT ( 'NONE',  ( -34.05310945292020364, 20.79694577634647246, 258.6823826759385270 ) ) ;
#5488=CARTESIAN_POINT ( 'NONE',  ( 172.0303573358525284, 20.79694577634646535, -196.1676464792605259 ) ) ;
#5492=ORIENTED_EDGE ( 'NONE', *, *, #10724, .T. ) ;
#5519=VECTOR ( 'NONE', #7465, 1000.000000000000227 ) ;
#5527=CARTESIAN_POINT ( 'NONE',  ( 261.1558126970361400, 19.96883746059272724, -17.09264059807959057 ) ) ;
#5547=CARTESIAN_POINT ( 'NONE',  ( 34.20858920406338655, 20.55460285047751157, -259.6535381481361355 ) ) ;
#5551=CARTESIAN_POINT ( 'NONE',  ( -258.6823826759384701, 20.79694577634646535, -34.05310945291999047 ) ) ;
#5561=CARTESIAN_POINT ( 'NONE',  ( -207.7919029844864269, 20.55460285060714654, 159.4136521835260112 ) ) ;
#5582=CONICAL_SURFACE ( 'NONE', #8997, 261.0000000000000000, 1.373400766945014784 ) ;
#5594=CARTESIAN_POINT ( 'NONE',  ( 247.8175805191053769, 19.96883746103348045, -84.14846197955421303 ) ) ;
#5615=CARTESIAN_POINT ( 'NONE',  ( -234.3927740973375080, 20.79694577663154575, -115.5625104413860100 ) ) ;
#5622=CARTESIAN_POINT ( 'NONE',  ( 115.4021059068220438, 20.79694577634646890, -234.0054343868617366 ) ) ;
#5628=( BOUNDED_CURVE ( )  B_SPLINE_CURVE ( 3, ( #2464, #12664, #9657, #10534 ),
 .UNSPECIFIED., .F., .F. ) 
 B_SPLINE_CURVE_WITH_KNOTS ( ( 4, 4 ),
 ( 0.000000000000000000, 1.000000000000000000 ),
 .UNSPECIFIED. ) 
 CURVE ( )  GEOMETRIC_REPRESENTATION_ITEM ( )  RATIONAL_B_SPLINE_CURVE ( ( 1.000000000000000000, 0.4027746460044325238, 0.4027746460044325238, 1.000000000000000000 ) ) 
 REPRESENTATION_ITEM ( '' )  );
#5646=DIRECTION ( 'NONE',  ( 0.000000000000000000, 0.000000000000000000, 1.000000000000000000 ) ) ;
#5660=CARTESIAN_POINT ( 'NONE',  ( 67.71318189755788808, 19.96883746081500988, -252.8031682274115894 ) ) ;
#5673=ORIENTED_EDGE ( 'NONE', *, *, #8441, .T. ) ;
#5680=CARTESIAN_POINT ( 'NONE',  ( -234.3927740981719978, 20.79694577626919028, 115.5625104415733944 ) ) ;
#5690=CARTESIAN_POINT ( 'NONE',  ( 211.9058003148608123, 20.08915143297736350, 151.8458048843642700 ) ) ;
#5707=DIRECTION ( 'NONE',  ( 0.000000000000000000, 0.000000000000000000, -1.000000000000000000 ) ) ;
#5725=CARTESIAN_POINT ( 'NONE',  ( 196.8887528220037950, 20.55460285134802589, -172.6991790960863966 ) ) ;
#5745=DIRECTION ( 'NONE',  ( 1.000000000000000000, -0.000000000000000000, 1.224646799147353207E-16 ) ) ;
#5748=CARTESIAN_POINT ( 'NONE',  ( -196.4640694359484883, 20.79694577636040265, -172.3268284091419957 ) ) ;
#5761=CARTESIAN_POINT ( 'NONE',  ( 178.2104428091926138, 20.08915143297736350, 190.2689011420771408 ) ) ;
#5766=CARTESIAN_POINT ( 'NONE',  ( -260.5542428346390125, 20.08915143307225648, 17.05314194216809653 ) ) ;
#5768=FACE_OUTER_BOUND ( 'NONE', #9200, .T. ) ;
#5782=CARTESIAN_POINT ( 'NONE',  ( -151.8458048843648101, 20.08915143297736705, 211.9058003148604143 ) ) ;
#5794=CARTESIAN_POINT ( 'NONE',  ( 17.10461161519311091, 20.55460285116648933, 261.3381329044966606 ) ) ;
#5806=EDGE_CURVE ( 'NONE', #8008, #3549, #7142, .T. ) ;
#5813=CARTESIAN_POINT ( 'NONE',  ( -130.5770120874175859, 20.08915143279216764, 226.1171533172259842 ) ) ;
#5818=CARTESIAN_POINT ( 'NONE',  ( 196.8887528220037950, 20.55460285134802589, -172.6991790960863966 ) ) ;
#5835=EDGE_CURVE ( 'NONE', #90, #953, #6719, .T. ) ;
#5842=ADVANCED_FACE ( 'NONE', ( #4733 ), #11076, .T. ) ;
#5853=CARTESIAN_POINT ( 'NONE',  ( -258.4638482596386098, 20.08915143297737060, -34.02434144668580274 ) ) ;
#5864=CARTESIAN_POINT ( 'NONE',  ( 261.3381329044966606, 20.55460285106647689, 17.10461161501256555 ) ) ;
#5885=CARTESIAN_POINT ( 'NONE',  ( -159.0697709846024850, 20.79694577629653551, -207.3438552932539949 ) ) ;
#5897=CARTESIAN_POINT ( 'NONE',  ( -226.1171533162824971, 20.08915143300168893, 130.5770120869439950 ) ) ;
#5910=DIRECTION ( 'NONE',  ( 0.000000000000000000, 0.000000000000000000, 1.000000000000000000 ) ) ;
#5920=ORIENTED_EDGE ( 'NONE', *, *, #2684, .F. ) ;
#5928=CARTESIAN_POINT ( 'NONE',  ( -67.76049180241520276, 20.55460285097757378, 252.9796497716870078 ) ) ;
#5968=CARTESIAN_POINT ( 'NONE',  ( 17.09264059789564172, 19.96883746058902176, -261.1558126970361400 ) ) ;
#5989=ORIENTED_EDGE ( 'NONE', *, *, #6531, .T. ) ;
#5997=CARTESIAN_POINT ( 'NONE',  ( 34.20858920311310669, 20.55460285062568815, 259.6535381495587558 ) ) ;
#6035=CARTESIAN_POINT ( 'NONE',  ( 258.8746690706130380, 20.08915143329827657, -34.10614053547809732 ) ) ;
#6062=CARTESIAN_POINT ( 'NONE',  ( 42.46883004693721375, 20.08915143297736705, -257.2112267038639288 ) ) ;
#6064=CARTESIAN_POINT ( 'NONE',  ( 115.5625104413773983, 20.79694577638496966, -234.3927740979615066 ) ) ;
#6079=CARTESIAN_POINT ( 'NONE',  ( -196.2980642837470100, 20.08915143287812199, -172.1812796682245050 ) ) ;
#6097=CARTESIAN_POINT ( 'NONE',  ( 172.1812796672219861, 20.08915143311016749, 196.2980642831085163 ) ) ;
#6102=CARTESIAN_POINT ( 'NONE',  ( 237.6585102388687289, 20.79694577634646890, 107.6783259591027644 ) ) ;
#6112=CARTESIAN_POINT ( 'NONE',  ( -130.4544329367273292, 20.79694577634646535, 225.9597979674042563 ) ) ;
#6122=CARTESIAN_POINT ( 'NONE',  ( -259.0935598604229995, 20.79694577620878704, -34.13493237027169158 ) ) ;
#6139=CARTESIAN_POINT ( 'NONE',  ( 252.2208631679629889, 20.08915143265645042, -67.55708173926119287 ) ) ;
#6145=CARTESIAN_POINT ( 'NONE',  ( 252.4341100441809829, 20.79694577595645910, -67.61424743030308093 ) ) ;
#6162=CARTESIAN_POINT ( 'NONE',  ( -115.7315435904061331, 19.96883746069636700, -234.7354397749499810 ) ) ;
#6181=DIRECTION ( 'NONE',  ( -1.224646799147349509E-16, 0.000000000000000000, -1.000000000000000000 ) ) ;
#6183=CARTESIAN_POINT ( 'NONE',  ( -234.0054343868616513, 20.79694577634646535, -115.4021059068222144 ) ) ;
#6193=CARTESIAN_POINT ( 'NONE',  ( 172.3268284089184874, 20.79694577645659948, 196.4640694358555209 ) ) ;
#6208=CARTESIAN_POINT ( 'NONE',  ( -247.2466869553009872, 20.08915143298854389, 83.95474316008009907 ) ) ;
#6214=AXIS2_PLACEMENT_3D ( 'NONE', #1710, #11907, #5707 ) ;
#6232=CARTESIAN_POINT ( 'NONE',  ( -226.6392846536229229, 19.96883746130017911, -130.8783844628770794 ) ) ;
#6237=EDGE_LOOP ( 'NONE', ( #4085, #289 ) ) ;
#6243=EDGE_CURVE ( 'NONE', #8825, #3483, #2436, .T. ) ;
#6250=CARTESIAN_POINT ( 'NONE',  ( -130.3442252640560923, 20.08915143297736705, -225.7689075324038299 ) ) ;
#6266=CARTESIAN_POINT ( 'NONE',  ( 247.4557548098379982, 20.79694577642534270, 84.02568524150230189 ) ) ;
#6277=CARTESIAN_POINT ( 'NONE',  ( 158.9353507248500250, 20.08915143321791419, 207.1687172302519855 ) ) ;
#6299=CARTESIAN_POINT ( 'NONE',  ( 159.3024069661366866, 19.96883746137792670, -207.6469600131167681 ) ) ;
#6305=CARTESIAN_POINT ( 'NONE',  ( 151.9741924115233189, 20.79694577634646180, 212.0849693193238181 ) ) ;
#6306=ORIENTED_EDGE ( 'NONE', *, *, #3516, .T. ) ;
#6327=CARTESIAN_POINT ( 'NONE',  ( 259.0935598591524922, 20.79694577673652134, -34.13493237036694694 ) ) ;
#6339=CARTESIAN_POINT ( 'NONE',  ( -252.2208631657525473, 20.08915143310922957, 67.55708173876999467 ) ) ;
#6348=DIRECTION ( 'NONE',  ( 0.000000000000000000, -1.000000000000000000, 0.000000000000000000 ) ) ;
#6360=CARTESIAN_POINT ( 'NONE',  ( -115.8123742918135832, 20.55460285136280518, 234.8993005745464586 ) ) ;
#6382=( GEOMETRIC_REPRESENTATION_CONTEXT ( 3 ) GLOBAL_UNCERTAINTY_ASSIGNED_CONTEXT ( ( #3973 ) ) GLOBAL_UNIT_ASSIGNED_CONTEXT ( ( #8905, #7243, #11307 ) ) REPRESENTATION_CONTEXT ( 'NONE', 'WORKASPACE' ) );
#6389=CARTESIAN_POINT ( 'NONE',  ( 258.4638482596385529, 20.08915143297736705, -34.02434144668546168 ) ) ;
#6406=CARTESIAN_POINT ( 'NONE',  ( 207.6469600143036587, 19.96883745899249618, -159.3024069668460072 ) ) ;
#6411=CARTESIAN_POINT ( 'NONE',  ( -8.533827019709523398, 20.79694577634646180, -260.7745447061711843 ) ) ;
#6426=CARTESIAN_POINT ( 'NONE',  ( -259.6535381484769118, 20.55460285079236016, -34.20858920326526942 ) ) ;
#6427=CARTESIAN_POINT ( 'NONE',  ( -107.5873595010537684, 20.08915143297736705, -237.4577367525705824 ) ) ;
#6433=CARTESIAN_POINT ( 'NONE',  ( -254.0989678903617914, 20.79694577634646535, -59.24444182677505211 ) ) ;
#6435=CARTESIAN_POINT ( 'NONE',  ( 212.0849693193239318, 20.79694577634646180, -151.9741924115230347 ) ) ;
#6455=CARTESIAN_POINT ( 'NONE',  ( 237.4577367525706109, 20.08915143297736705, -107.5873595010537542 ) ) ;
#6475=CARTESIAN_POINT ( 'NONE',  ( 130.8783844628973441, 19.96883745980737501, -226.6392846544037809 ) ) ;
#6479=CARTESIAN_POINT ( 'NONE',  ( -91.83222442980293465, 20.08915143297736705, 243.9837273761026779 ) ) ;
#6492=EDGE_CURVE ( 'NONE', #4809, #3483, #10137, .T. ) ;
#6496=CARTESIAN_POINT ( 'NONE',  ( 226.6392846536925276, 19.96883745972948176, 130.8783844628973441 ) ) ;
#6500=CARTESIAN_POINT ( 'NONE',  ( -178.3611219674587858, 20.79694577634646535, 190.4297758776776277 ) ) ;
#6504=CARTESIAN_POINT ( 'NONE',  ( 107.6783259591027786, 20.79694577634646535, -237.6585102388687289 ) ) ;
#6531=EDGE_CURVE ( 'NONE', #3706, #12702, #6943, .T. ) ;
#6536=CARTESIAN_POINT ( 'NONE',  ( 259.4723857435290597, 19.96883745944077404, 34.18476129351889625 ) ) ;
#6542=CARTESIAN_POINT ( 'NONE',  ( -115.3046144132258917, 20.08915143297736705, 233.8077470125388970 ) ) ;
#6557=CARTESIAN_POINT ( 'NONE',  ( 172.5787240287708073, 19.96883745935533838, 196.7513681801829932 ) ) ;
#6563=CARTESIAN_POINT ( 'NONE',  ( -83.86521783953236309, 20.79694577634646890, 247.0684411393754942 ) ) ;
#6565=CARTESIAN_POINT ( 'NONE',  ( 258.6823826759385838, 20.79694577634646890, -34.05310945291962099 ) ) ;
#6602=CARTESIAN_POINT ( 'NONE',  ( -261.1558126970361400, 19.96883746053716990, -17.09264059830048410 ) ) ;
#6609=B_SPLINE_CURVE_WITH_KNOTS ( 'NONE', 3,
 ( #8240, #11163, #3281, #11225, #10290, #10224, #5362, #1169, #9433, #2160, #5290, #12295, #5153, #6305, #168, #2031, #4222, #3344, #10354, #38, #1230, #8371, #9365, #10153, #6102, #12432, #304, #4359, #1028, #4093, #8172, #3088, #7166, #9612, #498, #6565, #2486, #2360, #1427, #12688, #4546, #4608, #3615, #11566, #8629, #6435, #9546, #3548, #365, #10497, #5488, #1365, #7620, #1558, #2423, #5622, #6504, #432, #8565, #7496, #6629, #12621, #4413, #11634, #8684, #10560 ),
 .UNSPECIFIED., .F., .F.,
 ( 4, 2, 2, 2, 2, 2, 2, 2, 2, 2, 2, 2, 2, 2, 2, 2, 2, 2, 2, 2, 2, 2, 2, 2, 2, 2, 2, 2, 2, 2, 2, 2, 4 ),
 ( 0.000000000000000000, 0.01562499999999998265, 0.03124999999999996531, 0.04687499999999994449, 0.06249999999999993061, 0.07812499999999991673, 0.09374999999999991673, 0.1093749999999999306, 0.1249999999999999445, 0.1406249999999999445, 0.1562499999999999722, 0.1718749999999999722, 0.1874999999999999722, 0.2031250000000000000, 0.2187500000000000000, 0.2343750000000000278, 0.2500000000000000555, 0.2656250000000000555, 0.2812500000000000000, 0.2968750000000000000, 0.3125000000000000000, 0.3281249999999999445, 0.3437499999999999445, 0.3593749999999999445, 0.3749999999999998890, 0.3906249999999998890, 0.4062499999999998890, 0.4218749999999998890, 0.4374999999999998890, 0.4531249999999999445, 0.4687500000000000000, 0.4843750000000000000, 0.5000000000000000000 ),
 .UNSPECIFIED. ) ;
#6622=CARTESIAN_POINT ( 'NONE',  ( 259.6535381495586421, 20.55460285116648578, 34.20858920465607156 ) ) ;
#6629=CARTESIAN_POINT ( 'NONE',  ( 59.24444182677506632, 20.79694577634646180, -254.0989678903618483 ) ) ;
#6641=CARTESIAN_POINT ( 'NONE',  ( -172.1812796675209825, 20.08915143307664053, -196.2980642830465001 ) ) ;
#6668=VERTEX_POINT ( 'NONE', #9663 ) ;
#6671=CARTESIAN_POINT ( 'NONE',  ( 67.71318189785222330, 19.96883746181513786, 252.8031682274115042 ) ) ;
#6692=CARTESIAN_POINT ( 'NONE',  ( 207.7919029858380213, 20.55460285149987953, -159.4136521842188188 ) ) ;
#6704=CARTESIAN_POINT ( 'NONE',  ( 260.1353576186481291, 20.08915143297736705, 17.05322212017798833 ) ) ;
#6708=CARTESIAN_POINT ( 'NONE',  ( -115.4648407707716018, 20.08915143296762906, -234.1947771733659920 ) ) ;
#6711=CARTESIAN_POINT ( 'NONE',  ( 0.000000000000000000, 0.000000000000000000, 0.000000000000000000 ) ) ;
#6714=ORIENTED_EDGE ( 'NONE', *, *, #6243, .T. ) ;
#6719=CIRCLE ( 'NONE', #10751, 3.000000000000002665 ) ;
#6720=DIRECTION ( 'NONE',  ( -0.000000000000000000, 1.000000000000000000, 0.000000000000000000 ) ) ;
#6736=CARTESIAN_POINT ( 'NONE',  ( -172.6991790971032970, 20.55460285072942384, -196.8887528238318509 ) ) ;
#6751=EDGE_LOOP ( 'NONE', ( #9333, #5177, #3166, #3104 ) ) ;
#6755=CARTESIAN_POINT ( 'NONE',  ( 115.8123742916068295, 20.55460285108873819, 234.8993005735927966 ) ) ;
#6765=CARTESIAN_POINT ( 'NONE',  ( 251.8100110699624281, 20.08915143297736705, 67.47543992452017392 ) ) ;
#6794=PRODUCT_DEFINITION_SHAPE ( 'NONE', 'NONE',  #8087 ) ;
#6798=CARTESIAN_POINT ( 'NONE',  ( 259.6535381495586421, 20.55460285116648578, 34.20858920465607156 ) ) ;
#6804=AXIS2_PLACEMENT_3D ( 'NONE', #8113, #7044, #1721 ) ;
#6816=CARTESIAN_POINT ( 'NONE',  ( -83.95474316043620888, 20.08915143278693094, 247.2466869562449858 ) ) ;
#6819=CARTESIAN_POINT ( 'NONE',  ( 17.06760680800665142, 20.79694577634646180, -260.7745447061710138 ) ) ;
#6832=CARTESIAN_POINT ( 'NONE',  ( -158.9353507248835058, 20.08915143316258778, 207.1687172305619811 ) ) ;
#6863=CARTESIAN_POINT ( 'NONE',  ( 130.9697226060475259, 20.55460285142580545, -226.7975291077671329 ) ) ;
#6879=CARTESIAN_POINT ( 'NONE',  ( 3.070225547948624535E-14, 19.00000000000000000, -250.7029414592220178 ) ) ;
#6883=CARTESIAN_POINT ( 'NONE',  ( 234.8993005740659044, 20.55460285055905700, 115.8123742914903289 ) ) ;
#6900=ORIENTED_EDGE ( 'NONE', *, *, #6492, .T. ) ;
#6902=CARTESIAN_POINT ( 'NONE',  ( -83.95474316043620888, 20.08915143278693094, 247.2466869562449858 ) ) ;
#6922=CARTESIAN_POINT ( 'NONE',  ( -158.8368823490021953, 20.79694577634646535, -206.9952515782969726 ) ) ;
#6930=CARTESIAN_POINT ( 'NONE',  ( 84.20717312453921011, 20.55460285117019126, -247.9906035365278001 ) ) ;
#6943=CIRCLE ( 'NONE', #1198, 246.0000000000000000 ) ;
#6947=DIRECTION ( 'NONE',  ( 1.224646799147349509E-16, 0.000000000000000000, -1.000000000000000000 ) ) ;
#6949=CARTESIAN_POINT ( 'NONE',  ( 34.13493237066314379, 20.79694577651677889, -259.0935598596149703 ) ) ;
#6950=CARTESIAN_POINT ( 'NONE',  ( 3.012631125902489062E-14, 21.99999999999995381, 246.0000000000000000 ) ) ;
#6964=CARTESIAN_POINT ( 'NONE',  ( -130.8783844633512956, 19.96883746151126360, 226.6392846543344035 ) ) ;
#6983=CARTESIAN_POINT ( 'NONE',  ( -212.0849693193236760, 20.79694577634646535, -151.9741924115234895 ) ) ;
#6991=CARTESIAN_POINT ( 'NONE',  ( 172.6991790965608971, 20.55460285089974093, 196.8887528236631965 ) ) ;
#7020=AXIS2_PLACEMENT_3D ( 'NONE', #5003, #3937, #634 ) ;
#7029=CARTESIAN_POINT ( 'NONE',  ( 258.8746690706134927, 20.08915143329815933, 34.10614053548034974 ) ) ;
#7032=( NAMED_UNIT ( * ) PLANE_ANGLE_UNIT ( ) SI_UNIT ( $, .RADIAN. ) );
#7044=DIRECTION ( 'NONE',  ( 0.000000000000000000, -1.000000000000000000, 0.000000000000000000 ) ) ;
#7046=CARTESIAN_POINT ( 'NONE',  ( -115.3046144132251527, 20.08915143297737060, -233.8077470125392949 ) ) ;
#7057=CARTESIAN_POINT ( 'NONE',  ( 17.05322212017823347, 20.08915143297737060, -260.1353576186481860 ) ) ;
#7060=CARTESIAN_POINT ( 'NONE',  ( -259.0935598604214647, 20.79694577620453799, 34.13493237032840000 ) ) ;
#7079=DIRECTION ( 'NONE',  ( 0.000000000000000000, -1.000000000000000000, 0.000000000000000000 ) ) ;
#7095=CARTESIAN_POINT ( 'NONE',  ( -252.8031682270705289, 19.96883745940372279, 67.71318189758537187 ) ) ;
#7114=CIRCLE ( 'NONE', #12638, 250.3823410207189966 ) ;
#7118=CARTESIAN_POINT ( 'NONE',  ( -257.4287020129719963, 20.79694577634646535, -42.50473797389778241 ) ) ;
#7129=CARTESIAN_POINT ( 'NONE',  ( -84.02568524183371323, 20.79694577604410100, 247.4557548106605225 ) ) ;
#7140=ORIENTED_EDGE ( 'NONE', *, *, #11862, .T. ) ;
#7142=CIRCLE ( 'NONE', #1602, 3.000000000000002665 ) ;
#7143=CARTESIAN_POINT ( 'NONE',  ( 260.5542428351129729, 20.08915143297737416, -17.05314194230804858 ) ) ;
#7147=CARTESIAN_POINT ( 'NONE',  ( 247.4557548098379982, 20.79694577642534270, 84.02568524150230189 ) ) ;
#7159=DIRECTION ( 'NONE',  ( 0.000000000000000000, -1.000000000000000000, 0.000000000000000000 ) ) ;
#7161=CARTESIAN_POINT ( 'NONE',  ( -207.6469600138974272, 19.96883745988519365, -159.3024069661565534 ) ) ;
#7166=CARTESIAN_POINT ( 'NONE',  ( 260.7745447061712412, 20.79694577634646890, 8.533827019709855577 ) ) ;
#7172=DIRECTION ( 'NONE',  ( 0.000000000000000000, -1.000000000000000000, 0.000000000000000000 ) ) ;
#7174=CARTESIAN_POINT ( 'NONE',  ( -158.7026972336032316, 20.08915143297737060, -206.8203823583193071 ) ) ;
#7177=CARTESIAN_POINT ( 'NONE',  ( -260.7745447061711843, 20.79694577634646535, -8.533827019710107820 ) ) ;
#7187=CARTESIAN_POINT ( 'NONE',  ( 226.3083638779000069, 20.79694577591247295, -130.6873781523096056 ) ) ;
#7198=CARTESIAN_POINT ( 'NONE',  ( 0.000000000000000000, 24.75600756274008063, 0.000000000000000000 ) ) ;
#7201=CARTESIAN_POINT ( 'NONE',  ( 83.95474316029249451, 20.08915143279689630, 247.2466869562504996 ) ) ;
#7230=CARTESIAN_POINT ( 'NONE',  ( 115.4648407705614090, 20.08915143315789109, 234.1947771724234713 ) ) ;
#7243=( NAMED_UNIT ( * ) PLANE_ANGLE_UNIT ( ) SI_UNIT ( $, .RADIAN. ) );
#7257=CARTESIAN_POINT ( 'NONE',  ( -67.61424743045878927, 20.79694577628127661, -252.4341100433800023 ) ) ;
#7260=AXIS2_PLACEMENT_3D ( 'NONE', #5448, #5383, #324 ) ;
#7270=CIRCLE ( 'NONE', #458, 3.000000000000002665 ) ;
#7272=CARTESIAN_POINT ( 'NONE',  ( 260.5542428351129729, 20.08915143297735284, 17.05314194231024771 ) ) ;
#7293=CARTESIAN_POINT ( 'NONE',  ( -226.7975291074607469, 20.55460285152577526, 130.9697226057901673 ) ) ;
#7321=CARTESIAN_POINT ( 'NONE',  ( 196.0019244007920918, 20.08915143297736350, 171.8850263962753218 ) ) ;
#7324=CARTESIAN_POINT ( 'NONE',  ( -159.0697709846024850, 20.79694577629653551, -207.3438552932539949 ) ) ;
#7335=CARTESIAN_POINT ( 'NONE',  ( 158.9353507265259964, 20.08915143275230974, -207.1687172319319927 ) ) ;
#7337=ADVANCED_FACE ( 'NONE', ( #4112, #8192 ), #12251, .F. ) ;
#7358=CARTESIAN_POINT ( 'NONE',  ( 259.4723857435290597, 19.96883745944077404, 34.18476129351889625 ) ) ;
#7363=CARTESIAN_POINT ( 'NONE',  ( 0.000000000000000000, 21.99999999999995381, -246.0000000000000000 ) ) ;
#7384=CARTESIAN_POINT ( 'NONE',  ( 107.5873595010541948, 20.08915143297735995, 237.4577367525702982 ) ) ;
#7397=CARTESIAN_POINT ( 'NONE',  ( 226.1171533156415023, 20.08915143315739726, 130.5770120865019805 ) ) ;
#7417=CARTESIAN_POINT ( 'NONE',  ( 207.6469600138280498, 19.96883746145561389, 159.3024069661363740 ) ) ;
#7420=CARTESIAN_POINT ( 'NONE',  ( 0.000000000000000000, 24.99999999999995737, 0.000000000000000000 ) ) ;
#7421=CARTESIAN_POINT ( 'NONE',  ( -8.533827019710209072, 20.79694577634647601, 260.7745447061713548 ) ) ;
#7449=CARTESIAN_POINT ( 'NONE',  ( 130.3442252640566039, 20.08915143297736705, -225.7689075324036025 ) ) ;
#7465=DIRECTION ( 'NONE',  ( 0.000000000000000000, -0.3950277506594045973, -0.9186691875800402363 ) ) ;
#7467=CARTESIAN_POINT ( 'NONE',  ( 84.14846197943569450, 19.96883746176665397, 247.8175805191055190 ) ) ;
#7488=CARTESIAN_POINT ( 'NONE',  ( -130.9697226053157237, 20.55460285097016282, -226.7975291069864738 ) ) ;
#7494=CARTESIAN_POINT ( 'NONE',  ( -234.0054343868620208, 20.79694577634646535, 115.4021059068214896 ) ) ;
#7496=CARTESIAN_POINT ( 'NONE',  ( 67.53249125288877508, 20.79694577634646180, -252.0229195836992062 ) ) ;
#7506=EDGE_CURVE ( 'NONE', #8008, #4210, #8175, .T. ) ;
#7517=CARTESIAN_POINT ( 'NONE',  ( 237.4577367525703835, 20.08915143297736350, 107.5873595010540669 ) ) ;
#7521=CONICAL_SURFACE ( 'NONE', #11132, 261.0000000000000000, 1.373400766945014784 ) ;
#7532=CARTESIAN_POINT ( 'NONE',  ( -67.71318189764485851, 19.96883746024804651, -252.8031682270704437 ) ) ;
#7537=CARTESIAN_POINT ( 'NONE',  ( -253.8843055347118707, 20.08915143297737060, -59.19439222780466991 ) ) ;
#7541=CARTESIAN_POINT ( 'NONE',  ( 0.000000000000000000, 24.99999999999995737, 0.000000000000000000 ) ) ;
#7545=EDGE_CURVE ( 'NONE', #1703, #90, #7114, .T. ) ;
#7553=CARTESIAN_POINT ( 'NONE',  ( -247.9906035374705766, 20.55460285117394648, 84.20717312385856701 ) ) ;
#7556=DIRECTION ( 'NONE',  ( 0.000000000000000000, 1.000000000000000000, 0.000000000000000000 ) ) ;
#7557=CARTESIAN_POINT ( 'NONE',  ( -4.572608844893758122E-13, 20.79694577634647601, 260.7745447061711275 ) ) ;
#7580=CARTESIAN_POINT ( 'NONE',  ( 0.000000000000000000, 21.99999999999995381, 0.000000000000000000 ) ) ;
#7592=CARTESIAN_POINT ( 'NONE',  ( -172.5787240293117293, 19.96883745935916821, -196.7513681803530403 ) ) ;
#7596=CARTESIAN_POINT ( 'NONE',  ( -251.8100110699625418, 20.08915143297736705, 67.47543992451960548 ) ) ;
#7612=CARTESIAN_POINT ( 'NONE',  ( 172.6991790965608971, 20.55460285089974093, 196.8887528236631965 ) ) ;
#7620=CARTESIAN_POINT ( 'NONE',  ( 151.9741924115233473, 20.79694577634646535, -212.0849693193237897 ) ) ;
#7655=CARTESIAN_POINT ( 'NONE',  ( 207.6469600138280498, 19.96883746145561389, 159.3024069661363740 ) ) ;
#7676=CARTESIAN_POINT ( 'NONE',  ( 259.6535381495593242, 20.55460285082940075, -34.20858920423904692 ) ) ;
#7694=CARTESIAN_POINT ( 'NONE',  ( 83.95474316006190918, 20.08915143290042948, -247.2466869557860036 ) ) ;
#7722=CARTESIAN_POINT ( 'NONE',  ( -261.3381329044966606, 20.55460285096646089, -17.10461161606123426 ) ) ;
#7747=CARTESIAN_POINT ( 'NONE',  ( -172.3268284098719789, 20.79694577634883856, 196.4640694352564765 ) ) ;
#7758=CARTESIAN_POINT ( 'NONE',  ( 67.47543992452030182, 20.08915143297736350, 251.8100110699621439 ) ) ;
#7759=ORIENTED_EDGE ( 'NONE', *, *, #4845, .T. ) ;
#7762=CARTESIAN_POINT ( 'NONE',  ( -115.4648407704221995, 20.08915143316778895, 234.1947771724274787 ) ) ;
#7779=EDGE_CURVE ( 'NONE', #3483, #8825, #6609, .T. ) ;
#7789=CARTESIAN_POINT ( 'NONE',  ( 234.8993005740659044, 20.55460285055905700, 115.8123742914903289 ) ) ;
#7805=CARTESIAN_POINT ( 'NONE',  ( -159.0697709836499882, 20.79694577635847352, 207.3438552937170130 ) ) ;
#7840=CARTESIAN_POINT ( 'NONE',  ( -260.1353576186481860, 20.08915143297736705, 17.05322212017742345 ) ) ;
#7855=CARTESIAN_POINT ( 'NONE',  ( 252.9796497720284094, 20.55460285130353881, -67.76049180262273808 ) ) ;
#7870=VECTOR ( 'NONE', #2265, 1000.000000000000000 ) ;
#7875=CARTESIAN_POINT ( 'NONE',  ( 130.9697226058085846, 20.55460285117392516, 226.7975291051602937 ) ) ;
#7887=AXIS2_PLACEMENT_3D ( 'NONE', #2406, #10542, #8546 ) ;
#7896=EDGE_LOOP ( 'NONE', ( #126, #8373, #12350, #9892 ) ) ;
#7910=CARTESIAN_POINT ( 'NONE',  ( 260.5542428351129729, 20.08915143297737416, -17.05314194230804858 ) ) ;
#7921=CARTESIAN_POINT ( 'NONE',  ( 84.20717312394452847, 20.55460285104429019, 247.9906035367661161 ) ) ;
#7941=DIRECTION ( 'NONE',  ( 0.000000000000000000, 0.000000000000000000, 1.000000000000000000 ) ) ;
#7945=CARTESIAN_POINT ( 'NONE',  ( 115.5625104412701916, 20.79694577657783228, 234.3927740975209986 ) ) ;
#7955=UNCERTAINTY_MEASURE_WITH_UNIT (LENGTH_MEASURE( 1.000000000000000082E-05 ), #11965, 'distance_accuracy_value', 'NONE');
#7965=CARTESIAN_POINT ( 'NONE',  ( -159.3024069663917146, 19.96883746063718590, -207.6469600136618681 ) ) ;
#7968=AXIS2_PLACEMENT_3D ( 'NONE', #8896, #9749, #8832 ) ;
#7981=CARTESIAN_POINT ( 'NONE',  ( -178.2104428091931823, 20.08915143297737060, 190.2689011420768850 ) ) ;
#7995=CARTESIAN_POINT ( 'NONE',  ( -252.9796497731091165, 20.55460285134058651, -67.76049180360037383 ) ) ;
#8006=VECTOR ( 'NONE', #11079, 1000.000000000000227 ) ;
#8008=VERTEX_POINT ( 'NONE', #275 ) ;
#8029=CARTESIAN_POINT ( 'NONE',  ( -196.7513681794031868, 19.96883746182613706, -172.5787240283650590 ) ) ;
#8037=ORIENTED_EDGE ( 'NONE', *, *, #4669, .T. ) ;
#8044=FACE_OUTER_BOUND ( 'NONE', #3109, .T. ) ;
#8057=CARTESIAN_POINT ( 'NONE',  ( -226.3083638767344894, 20.79694577654763421, 130.6873781513949950 ) ) ;
#8077=EDGE_CURVE ( 'NONE', #6668, #2888, #2926, .T. ) ;
#8087=PRODUCT_DEFINITION ( 'UNKNOWN', '', #13006, #11017 ) ;
#8098=CARTESIAN_POINT ( 'NONE',  ( -1.008906662707803564E-12, 19.96883746059272724, 261.1558126970361400 ) ) ;
#8100=CARTESIAN_POINT ( 'NONE',  ( 0.000000000000000000, 20.00000000000000000, 0.000000000000000000 ) ) ;
#8113=CARTESIAN_POINT ( 'NONE',  ( 0.000000000000000000, 21.99999999999995381, 0.000000000000000000 ) ) ;
#8115=CARTESIAN_POINT ( 'NONE',  ( -196.0019244007917791, 20.08915143297737060, -171.8850263962756912 ) ) ;
#8131=CARTESIAN_POINT ( 'NONE',  ( 234.3927740981229988, 20.79694577626769103, 115.5625104417014057 ) ) ;
#8145=CARTESIAN_POINT ( 'NONE',  ( -115.4648407707716018, 20.08915143296762906, -234.1947771733659920 ) ) ;
#8167=CARTESIAN_POINT ( 'NONE',  ( -159.3024069656823940, 19.96883745967399548, 207.6469600131863729 ) ) ;
#8172=CARTESIAN_POINT ( 'NONE',  ( 258.6823826759384701, 20.79694577634646890, 34.05310945291972757 ) ) ;
#8175=CIRCLE ( 'NONE', #2414, 251.2912898646364397 ) ;
#8186=EDGE_CURVE ( 'NONE', #1703, #4809, #10954, .T. ) ;
#8192=FACE_OUTER_BOUND ( 'NONE', #1815, .T. ) ;
#8200=CARTESIAN_POINT ( 'NONE',  ( -234.3927740981719978, 20.79694577626919028, 115.5625104415733944 ) ) ;
#8213=ORIENTED_EDGE ( 'NONE', *, *, #2109, .F. ) ;
#8216=CARTESIAN_POINT ( 'NONE',  ( 172.1812796676979929, 20.08915143304314910, -196.2980642831070099 ) ) ;
#8235=CARTESIAN_POINT ( 'NONE',  ( 84.14846197979342435, 19.96883746137058679, -247.8175805188673735 ) ) ;
#8240=CARTESIAN_POINT ( 'NONE',  ( -4.572608844893758122E-13, 20.79694577634647601, 260.7745447061711275 ) ) ;
#8251=CARTESIAN_POINT ( 'NONE',  ( -42.46883004693665953, 20.08915143297737060, -257.2112267038640425 ) ) ;
#8263=CARTESIAN_POINT ( 'NONE',  ( -34.13493237016224668, 20.79694577639865471, 259.0935598599945138 ) ) ;
#8277=CARTESIAN_POINT ( 'NONE',  ( -158.9353507248835058, 20.08915143316258778, 207.1687172305619811 ) ) ;
#8286=DIRECTION ( 'NONE',  ( 0.000000000000000000, -1.000000000000000000, 0.000000000000000000 ) ) ;
#8300=CARTESIAN_POINT ( 'NONE',  ( 196.7513681799443361, 19.96883746182971464, 172.5787240285351345 ) ) ;
#8330=CARTESIAN_POINT ( 'NONE',  ( -252.4341100429120104, 20.79694577648844245, 67.61424743034129392 ) ) ;
#8343=CARTESIAN_POINT ( 'NONE',  ( -84.14846197923118609, 19.96883746246331981, 247.8175805181506348 ) ) ;
#8363=CARTESIAN_POINT ( 'NONE',  ( 67.71318189785222330, 19.96883746181513786, 252.8031682274115042 ) ) ;
#8371=CARTESIAN_POINT ( 'NONE',  ( 221.5672498511021047, 20.79694577634646890, 137.7829567244531574 ) ) ;
#8373=ORIENTED_EDGE ( 'NONE', *, *, #8746, .T. ) ;
#8385=AXIS2_PLACEMENT_3D ( 'NONE', #10572, #641, #4693 ) ;
#8392=CARTESIAN_POINT ( 'NONE',  ( 253.8843055347119275, 20.08915143297736705, -59.19439222780434307 ) ) ;
#8406=CARTESIAN_POINT ( 'NONE',  ( 252.2208631679619941, 20.08915143265656766, 67.55708173926319660 ) ) ;
#8414=ADVANCED_FACE ( 'NONE', ( #5768 ), #2839, .T. ) ;
#8429=CARTESIAN_POINT ( 'NONE',  ( -234.8993005728878529, 20.55460285095910677, 115.8123742916932741 ) ) ;
#8435=CARTESIAN_POINT ( 'NONE',  ( -244.1900186690936323, 20.79694577634646180, 91.90986972409903899 ) ) ;
#8441=EDGE_CURVE ( 'NONE', #3706, #10670, #1700, .T. ) ;
#8443=SHAPE_REPRESENTATION ( 'Slewing Ring High Pressure Lip Seals Top', ( #805 ), #391 ) ;
#8460=CARTESIAN_POINT ( 'NONE',  ( 243.9837273761028769, 20.08915143297736705, 91.83222442980245148 ) ) ;
#8462=FACE_OUTER_BOUND ( 'NONE', #11831, .T. ) ;
#8471=CARTESIAN_POINT ( 'NONE',  ( 159.3024069666089133, 19.96883745889249795, 207.6469600140662806 ) ) ;
#8492=CARTESIAN_POINT ( 'NONE',  ( -207.7919029851962023, 20.55460285100346596, -159.4136521840017906 ) ) ;
#8496=CARTESIAN_POINT ( 'NONE',  ( -225.9597979674045973, 20.79694577634646535, 130.4544329367265334 ) ) ;
#8521=CARTESIAN_POINT ( 'NONE',  ( 243.9837273761030474, 20.08915143297736705, -91.83222442980216726 ) ) ;
#8537=CARTESIAN_POINT ( 'NONE',  ( 226.6392846532197325, 19.96883746219288724, -130.8783844621844707 ) ) ;
#8541=ORIENTED_EDGE ( 'NONE', *, *, #5806, .T. ) ;
#8542=CARTESIAN_POINT ( 'NONE',  ( -260.5542428351132003, 20.08915143297736705, 8.526617657837524789 ) ) ;
#8546=DIRECTION ( 'NONE',  ( 0.000000000000000000, 0.000000000000000000, 1.000000000000000000 ) ) ;
#8555=CARTESIAN_POINT ( 'NONE',  ( -261.3381329044966606, 20.55460285116648933, 17.10461161605900671 ) ) ;
#8562=CARTESIAN_POINT ( 'NONE',  ( -42.50473797389807373, 20.79694577634647246, 257.4287020129720531 ) ) ;
#8563=ADVANCED_FACE ( 'NONE', ( #3013 ), #5582, .F. ) ;
#8565=CARTESIAN_POINT ( 'NONE',  ( 83.86521783953205045, 20.79694577634646180, -247.0684411393754942 ) ) ;
#8601=CARTESIAN_POINT ( 'NONE',  ( 261.1558126970361400, 19.96883746059272724, 17.09264059808175062 ) ) ;
#8607=CARTESIAN_POINT ( 'NONE',  ( -42.46883004693748376, 20.08915143297736705, 257.2112267038638720 ) ) ;
#8622=CARTESIAN_POINT ( 'NONE',  ( -115.5625104412419972, 20.79694577648909615, -234.3927740977559893 ) ) ;
#8626=CARTESIAN_POINT ( 'NONE',  ( -212.0849693193241592, 20.79694577634646535, 151.9741924115227789 ) ) ;
#8629=CARTESIAN_POINT ( 'NONE',  ( 221.5672498511021331, 20.79694577634646890, -137.7829567244531006 ) ) ;
#8633=VERTEX_POINT ( 'NONE', #5284 ) ;
#8636=FACE_OUTER_BOUND ( 'NONE', #2613, .T. ) ;
#8660=CARTESIAN_POINT ( 'NONE',  ( 234.7354397751814759, 19.96883746015188876, -115.7315435904363312 ) ) ;
#8672=CARTESIAN_POINT ( 'NONE',  ( 1.104728353688762803E-12, 19.96883746059272724, -261.1558126970361400 ) ) ;
#8677=CARTESIAN_POINT ( 'NONE',  ( 159.4136521832723474, 20.55460285070720161, -207.7919029841772840 ) ) ;
#8684=CARTESIAN_POINT ( 'NONE',  ( 8.533827019709857353, 20.79694577634646535, -260.7745447061712980 ) ) ;
#8693=CARTESIAN_POINT ( 'NONE',  ( 67.55708173896789503, 20.08915143276009729, -252.2208631674930359 ) ) ;
#8728=CARTESIAN_POINT ( 'NONE',  ( -17.09264059789343193, 19.96883746059643983, -261.1558126970361400 ) ) ;
#8746=EDGE_CURVE ( 'NONE', #4210, #6668, #164, .T. ) ;
#8747=CARTESIAN_POINT ( 'NONE',  ( -247.4557548106230058, 20.79694577606145600, -84.02568524181840814 ) ) ;
#8757=CARTESIAN_POINT ( 'NONE',  ( 130.3442252640560639, 20.08915143297736705, 225.7689075324037731 ) ) ;
#8763=CARTESIAN_POINT ( 'NONE',  ( -67.55708173894439028, 20.08915143292001204, -252.2208631666825056 ) ) ;
#8792=CARTESIAN_POINT ( 'NONE',  ( 261.3381329044966606, 20.55460285106647689, -17.10461161501038063 ) ) ;
#8815=CARTESIAN_POINT ( 'NONE',  ( -260.7745447066434963, 20.79694577614318618, -17.06760680913714978 ) ) ;
#8825=VERTEX_POINT ( 'NONE', #1551 ) ;
#8826=CARTESIAN_POINT ( 'NONE',  ( 233.8077470125390676, 20.08915143297735995, -115.3046144132253374 ) ) ;
#8830=CARTESIAN_POINT ( 'NONE',  ( -258.8746690723625079, 20.08915143294039396, -34.10614053585524630 ) ) ;
#8832=DIRECTION ( 'NONE',  ( 0.000000000000000000, 0.000000000000000000, -1.000000000000000000 ) ) ;
#8848=CARTESIAN_POINT ( 'NONE',  ( -196.0019244007923476, 20.08915143297736705, 171.8850263962750660 ) ) ;
#8860=CARTESIAN_POINT ( 'NONE',  ( -34.20858920326337227, 20.55460285088512506, -259.6535381484778782 ) ) ;
#8876=CARTESIAN_POINT ( 'NONE',  ( -130.6873781523279945, 20.79694577633451402, 226.3083638767075172 ) ) ;
#8895=CARTESIAN_POINT ( 'NONE',  ( -207.1687172310330141, 20.08915143305816997, -158.9353507251184965 ) ) ;
#8896=CARTESIAN_POINT ( 'NONE',  ( 0.000000000000000000, 21.99999999999995381, 0.000000000000000000 ) ) ;
#8905=( LENGTH_UNIT ( ) NAMED_UNIT ( * ) SI_UNIT ( .MILLI., .METRE. ) );
#8915=CARTESIAN_POINT ( 'NONE',  ( -251.8100110699623144, 20.08915143297736705, -67.47543992452018813 ) ) ;
#8918=CARTESIAN_POINT ( 'NONE',  ( -130.4544329367265902, 20.79694577634646535, -225.9597979674047110 ) ) ;
#8927=CARTESIAN_POINT ( 'NONE',  ( 115.8123742910162264, 20.55460285096275541, -234.8993005738286115 ) ) ;
#8949=CARTESIAN_POINT ( 'NONE',  ( 67.61424743078299571, 20.79694577590440119, 252.4341100442090067 ) ) ;
#8964=CARTESIAN_POINT ( 'NONE',  ( -252.2208631657525473, 20.08915143310922957, 67.55708173876999467 ) ) ;
#8980=CARTESIAN_POINT ( 'NONE',  ( -67.47543992452052919, 20.08915143297736705, 251.8100110699622576 ) ) ;
#8982=CARTESIAN_POINT ( 'NONE',  ( -190.4297758776777130, 20.79694577634646535, -178.3611219674585584 ) ) ;
#8994=CARTESIAN_POINT ( 'NONE',  ( 207.7919029858380213, 20.55460285149987953, -159.4136521842188188 ) ) ;
#8997=AXIS2_PLACEMENT_3D ( 'NONE', #8100, #2950, #12092 ) ;
#9031=CARTESIAN_POINT ( 'NONE',  ( -261.1558126970361400, 19.96883746064829168, 17.09264059829825300 ) ) ;
#9039=VERTEX_POINT ( 'NONE', #6950 ) ;
#9041=CARTESIAN_POINT ( 'NONE',  ( 0.000000000000000000, 22.00000000000000000, 0.000000000000000000 ) ) ;
#9058=CARTESIAN_POINT ( 'NONE',  ( 226.7975291061089820, 20.55460285063310621, -130.9697226050975019 ) ) ;
#9092=CARTESIAN_POINT ( 'NONE',  ( 226.1171533156415023, 20.08915143315739726, 130.5770120865019805 ) ) ;
#9106=CARTESIAN_POINT ( 'NONE',  ( -59.19439222780410148, 20.08915143297736705, -253.8843055347119275 ) ) ;
#9119=CARTESIAN_POINT ( 'NONE',  ( 115.5625104412701916, 20.79694577657783228, 234.3927740975209986 ) ) ;
#9136=CARTESIAN_POINT ( 'NONE',  ( 234.1947771726669885, 20.08915143309429041, 115.4648407708036046 ) ) ;
#9157=CARTESIAN_POINT ( 'NONE',  ( -84.14846197923118609, 19.96883746246331981, 247.8175805181506348 ) ) ;
#9164=ORIENTED_EDGE ( 'NONE', *, *, #8186, .F. ) ;
#9168=ADVANCED_FACE ( 'NONE', ( #5005 ), #7521, .F. ) ;
#9190=CARTESIAN_POINT ( 'NONE',  ( -115.5625104412419972, 20.79694577648909615, -234.3927740977559893 ) ) ;
#9194=CARTESIAN_POINT ( 'NONE',  ( 172.3268284095375122, 20.79694577629726027, -196.4640694357605071 ) ) ;
#9200=EDGE_LOOP ( 'NONE', ( #3298, #11780, #5158, #12731 ) ) ;
#9203=CARTESIAN_POINT ( 'NONE',  ( 226.1171533175249806, 20.08915143274010262, -130.5770120874387885 ) ) ;
#9208=CARTESIAN_POINT ( 'NONE',  ( 196.4640694355999813, 20.79694577639575570, -172.3268284093740021 ) ) ;
#9216=FACE_OUTER_BOUND ( 'NONE', #3562, .T. ) ;
#9222=CARTESIAN_POINT ( 'NONE',  ( 0.000000000000000000, 24.99999999999995737, -250.3823410207189966 ) ) ;
#9227=CARTESIAN_POINT ( 'NONE',  ( 67.71318189755788808, 19.96883746081500988, -252.8031682274115894 ) ) ;
#9247=CARTESIAN_POINT ( 'NONE',  ( -190.4297758776781393, 20.79694577634646180, 178.3611219674581037 ) ) ;
#9259=CARTESIAN_POINT ( 'NONE',  ( -34.13493237021134519, 20.79694577641179620, -259.0935598599534728 ) ) ;
#9273=CARTESIAN_POINT ( 'NONE',  ( -172.1812796675209825, 20.08915143307664053, -196.2980642830465001 ) ) ;
#9291=CARTESIAN_POINT ( 'NONE',  ( 234.1947771728840166, 20.08915143305504714, -115.4648407707930033 ) ) ;
#9303=ADVANCED_FACE ( 'NONE', ( #5469 ), #3392, .F. ) ;
#9307=DIRECTION ( 'NONE',  ( 0.000000000000000000, 0.000000000000000000, -1.000000000000000000 ) ) ;
#9308=CARTESIAN_POINT ( 'NONE',  ( -178.2104428091925854, 20.08915143297736350, -190.2689011420772260 ) ) ;
#9320=CARTESIAN_POINT ( 'NONE',  ( 260.7745447061710138, 20.79694577634646180, 17.06760680878259961 ) ) ;
#9333=ORIENTED_EDGE ( 'NONE', *, *, #5016, .F. ) ;
#9334=CARTESIAN_POINT ( 'NONE',  ( -1.008906662707803564E-12, 19.96883746059272724, 261.1558126970361400 ) ) ;
#9359=CARTESIAN_POINT ( 'NONE',  ( -17.10461161519512174, 20.55460285096646089, 261.3381329044966606 ) ) ;
#9365=CARTESIAN_POINT ( 'NONE',  ( 225.9597979674045405, 20.79694577634646535, 130.4544329367268460 ) ) ;
#9386=CARTESIAN_POINT ( 'NONE',  ( 260.5542428351133140, 20.08915143297737060, -8.526617657837807229 ) ) ;
#9389=CARTESIAN_POINT ( 'NONE',  ( -172.3268284091859925, 20.79694577633260621, -196.4640694359954978 ) ) ;
#9402=CARTESIAN_POINT ( 'NONE',  ( 196.2980642840460064, 20.08915143284461280, 172.1812796681624889 ) ) ;
#9410=DIRECTION ( 'NONE',  ( 0.000000000000000000, 0.000000000000000000, -1.000000000000000000 ) ) ;
#9425=CIRCLE ( 'NONE', #9839, 251.5674242726969680 ) ;
#9427=CARTESIAN_POINT ( 'NONE',  ( -159.4136521825795114, 20.55460285040709678, 207.7919029861446916 ) ) ;
#9433=CARTESIAN_POINT ( 'NONE',  ( 91.90986972409980638, 20.79694577634647246, 244.1900186690935470 ) ) ;
#9454=CARTESIAN_POINT ( 'NONE',  ( 260.5542428351132571, 20.08915143297736705, 8.526617657838089670 ) ) ;
#9468=CARTESIAN_POINT ( 'NONE',  ( 252.8031682264634981, 19.96883746174475860, 67.71318189738019555 ) ) ;
#9487=CARTESIAN_POINT ( 'NONE',  ( -234.8993005735983104, 20.55460285152947009, -115.8123742918138248 ) ) ;
#9498=CARTESIAN_POINT ( 'NONE',  ( 6.345753394971347358E-13, 20.08915143297736350, -260.5542428351130866 ) ) ;
#9511=CARTESIAN_POINT ( 'NONE',  ( 257.2112267038638151, 20.08915143297736350, -42.46883004693691532 ) ) ;
#9522=CARTESIAN_POINT ( 'NONE',  ( -115.7315435907638346, 19.96883745872212046, 234.7354397761344273 ) ) ;
#9527=CARTESIAN_POINT ( 'NONE',  ( -206.8203823583193639, 20.08915143297736350, 158.7026972336029758 ) ) ;
#9532=CARTESIAN_POINT ( 'NONE',  ( 1.091807554230414677E-12, 20.55460285106647689, -261.3381329044966606 ) ) ;
#9534=ORIENTED_EDGE ( 'NONE', *, *, #8077, .F. ) ;
#9540=CARTESIAN_POINT ( 'NONE',  ( 17.10461161403171815, 20.55460285106647689, -261.3381329044966606 ) ) ;
#9544=CARTESIAN_POINT ( 'NONE',  ( -91.90986972410016165, 20.79694577634646890, 244.1900186690933765 ) ) ;
#9546=CARTESIAN_POINT ( 'NONE',  ( 206.9952515782969158, 20.79694577634646890, -158.8368823490023374 ) ) ;
#9572=AXIS2_PLACEMENT_3D ( 'NONE', #7580, #520, #9634 ) ;
#9585=CARTESIAN_POINT ( 'NONE',  ( 234.7354397747064354, 19.96883745941838484, 115.7315435904383349 ) ) ;
#9590=CARTESIAN_POINT ( 'NONE',  ( -8.526617657838487574, 20.08915143297736705, 260.5542428351131434 ) ) ;
#9597=DIRECTION ( 'NONE',  ( -1.000000000000000000, -0.000000000000000000, -0.000000000000000000 ) ) ;
#9603=CARTESIAN_POINT ( 'NONE',  ( -17.10461161402953323, 20.55460285106647689, -261.3381329044966606 ) ) ;
#9609=CARTESIAN_POINT ( 'NONE',  ( -260.3553053170167004, 20.79694577634646535, 17.06764083276396704 ) ) ;
#9611=ADVANCED_FACE ( 'NONE', ( #8044 ), #3224, .T. ) ;
#9612=CARTESIAN_POINT ( 'NONE',  ( 260.7745447061712412, 20.79694577634646890, -8.533827019709542938 ) ) ;
#9634=DIRECTION ( 'NONE',  ( 0.000000000000000000, 0.000000000000000000, -1.000000000000000000 ) ) ;
#9654=CARTESIAN_POINT ( 'NONE',  ( -172.5787240286020392, 19.96883746144090210, 196.7513681798772609 ) ) ;
#9657=CARTESIAN_POINT ( 'NONE',  ( -1.009183486025028462E-12, 20.55460285106647689, 261.3381329044966606 ) ) ;
#9663=CARTESIAN_POINT ( 'NONE',  ( -7.780566028168587395E-13, 20.08915143297736350, 260.5542428351130866 ) ) ;
#9673=CARTESIAN_POINT ( 'NONE',  ( -207.3438552930580272, 20.79694577641581077, -159.0697709843959728 ) ) ;
#9690=CARTESIAN_POINT ( 'NONE',  ( 17.05314194221880086, 20.08915143297735284, -260.5542428351129729 ) ) ;
#9712=CARTESIAN_POINT ( 'NONE',  ( -196.7513681794031868, 19.96883746182613706, -172.5787240283650590 ) ) ;
#9732=CARTESIAN_POINT ( 'NONE',  ( -259.0935598604214647, 20.79694577620453799, 34.13493237032840000 ) ) ;
#9743=CARTESIAN_POINT ( 'NONE',  ( 151.8458048843644690, 20.08915143297736705, 211.9058003148607270 ) ) ;
#9749=DIRECTION ( 'NONE',  ( 0.000000000000000000, -1.000000000000000000, 0.000000000000000000 ) ) ;
#9783=CARTESIAN_POINT ( 'NONE',  ( -226.7975291067479588, 20.55460285112940610, -130.9697226053176564 ) ) ;
#9804=CARTESIAN_POINT ( 'NONE',  ( -172.3268284091859925, 20.79694577633260621, -196.4640694359954978 ) ) ;
#9819=CARTESIAN_POINT ( 'NONE',  ( 17.05322212017792793, 20.08915143297736705, 260.1353576186482428 ) ) ;
#9839=AXIS2_PLACEMENT_3D ( 'NONE', #7198, #2197, #2259 ) ;
#9841=CARTESIAN_POINT ( 'NONE',  ( -225.7689075324038583, 20.08915143297736705, 130.3442252640560639 ) ) ;
#9855=CARTESIAN_POINT ( 'NONE',  ( -172.6991790963936921, 20.55460285138878618, 196.8887528212225106 ) ) ;
#9879=CARTESIAN_POINT ( 'NONE',  ( 234.8993005733554185, 20.55460285121469610, -115.8123742911327838 ) ) ;
#9892=ORIENTED_EDGE ( 'NONE', *, *, #3516, .F. ) ;
#9911=CARTESIAN_POINT ( 'NONE',  ( -243.9837273761031042, 20.08915143297736705, 91.83222442980193989 ) ) ;
#9923=CARTESIAN_POINT ( 'NONE',  ( 130.9697226058085846, 20.55460285117392516, 226.7975291051602937 ) ) ;
#9938=CARTESIAN_POINT ( 'NONE',  ( 247.4557548102664839, 20.79694577621951979, -84.02568524171830688 ) ) ;
#9958=CARTESIAN_POINT ( 'NONE',  ( 0.000000000000000000, 23.50000000000000000, -246.0000000000000000 ) ) ;
#9977=CARTESIAN_POINT ( 'NONE',  ( -34.02434144668606564, 20.08915143297736705, 258.4638482596384961 ) ) ;
#9981=ADVANCED_FACE ( 'NONE', ( #635 ), #12447, .T. ) ;
#9992=CARTESIAN_POINT ( 'NONE',  ( -159.4136521825795114, 20.55460285040709678, 207.7919029861446916 ) ) ;
#10008=CARTESIAN_POINT ( 'NONE',  ( -17.05314194195814892, 20.08915143288246696, 260.5542428355875018 ) ) ;
#10010=CARTESIAN_POINT ( 'NONE',  ( 260.7745447061710138, 20.79694577634651509, -17.06760680878044667 ) ) ;
#10024=CARTESIAN_POINT ( 'NONE',  ( 83.95474316029249451, 20.08915143279689630, 247.2466869562504996 ) ) ;
#10045=CARTESIAN_POINT ( 'NONE',  ( -196.1676464792605259, 20.79694577634646535, -172.0303573358525000 ) ) ;
#10055=CARTESIAN_POINT ( 'NONE',  ( -1.009183486025028462E-12, 20.55460285106647689, 261.3381329044966606 ) ) ;
#10078=AXIS2_PLACEMENT_3D ( 'NONE', #7420, #7556, #3544 ) ;
#10090=CARTESIAN_POINT ( 'NONE',  ( 172.1812796676979929, 20.08915143304314910, -196.2980642831070099 ) ) ;
#10117=CARTESIAN_POINT ( 'NONE',  ( 130.6873781525580114, 20.79694577610125705, 226.3083638772055224 ) ) ;
#10131=CARTESIAN_POINT ( 'NONE',  ( -196.2980642832790181, 20.08915143307791951, 172.1812796672794832 ) ) ;
#10137=LINE ( 'NONE', #1011, #8006 ) ;
#10148=CARTESIAN_POINT ( 'NONE',  ( -226.6392846543355688, 19.96883746039994278, 130.8783844631124680 ) ) ;
#10153=CARTESIAN_POINT ( 'NONE',  ( 234.0054343868618503, 20.79694577634646180, 115.4021059068217596 ) ) ;
#10162=CARTESIAN_POINT ( 'NONE',  ( -243.9837273761027916, 20.08915143297736705, -91.83222442980269307 ) ) ;
#10165=CARTESIAN_POINT ( 'NONE',  ( -107.6783259591032333, 20.79694577634646535, 237.6585102388684732 ) ) ;
#10177=CARTESIAN_POINT ( 'NONE',  ( -226.3083638773660198, 20.79694577627718388, -130.6873781515817825 ) ) ;
#10194=CARTESIAN_POINT ( 'NONE',  ( -258.8746690728235080, 20.08915143284549387, 34.10614053596890471 ) ) ;
#10201=CARTESIAN_POINT ( 'NONE',  ( 259.0935598591524922, 20.79694577673652134, -34.13493237036694694 ) ) ;
#10202=DIRECTION ( 'NONE',  ( 0.000000000000000000, 0.000000000000000000, -1.000000000000000000 ) ) ;
#10217=CARTESIAN_POINT ( 'NONE',  ( -84.14846197958475216, 19.96883746048893471, -247.8175805193368717 ) ) ;
#10224=CARTESIAN_POINT ( 'NONE',  ( 59.24444182677519422, 20.79694577634646535, 254.0989678903617346 ) ) ;
#10236=CARTESIAN_POINT ( 'NONE',  ( -258.6823826759385270, 20.79694577634646535, 34.05310945291919467 ) ) ;
#10244=CARTESIAN_POINT ( 'NONE',  ( 8.526617657838109210, 20.08915143297737060, -260.5542428351132571 ) ) ;
#10247=CARTESIAN_POINT ( 'NONE',  ( -17.06760680800445229, 20.79694577634651509, -260.7745447061710138 ) ) ;
#10261=CARTESIAN_POINT ( 'NONE',  ( -234.1947771728870009, 20.08915143306511553, -115.4648407706533959 ) ) ;
#10262=CARTESIAN_POINT ( 'NONE',  ( 0.000000000000000000, 24.99999999999995737, 0.000000000000000000 ) ) ;
#10284=CARTESIAN_POINT ( 'NONE',  ( -115.7315435907638346, 19.96883745872212046, 234.7354397761344273 ) ) ;
#10290=CARTESIAN_POINT ( 'NONE',  ( 42.50473797389793873, 20.79694577634646535, 257.4287020129719394 ) ) ;
#10302=CARTESIAN_POINT ( 'NONE',  ( -237.4577367525703266, 20.08915143297737060, -107.5873595010543511 ) ) ;
#10315=CARTESIAN_POINT ( 'NONE',  ( 130.6873781507030117, 20.79694577677803125, -226.3083638765525052 ) ) ;
#10328=CARTESIAN_POINT ( 'NONE',  ( -260.5542428355875018, 20.08915143288246696, -17.05314194217034895 ) ) ;
#10340=ORIENTED_EDGE ( 'NONE', *, *, #2570, .F. ) ;
#10348=CARTESIAN_POINT ( 'NONE',  ( 259.4723857435292302, 19.96883745945557820, -34.18476129351679305 ) ) ;
#10354=CARTESIAN_POINT ( 'NONE',  ( 196.1676464792608670, 20.79694577634646535, 172.0303573358521589 ) ) ;
#10375=CARTESIAN_POINT ( 'NONE',  ( 151.8458048843644690, 20.08915143297736705, -211.9058003148606417 ) ) ;
#10377=CARTESIAN_POINT ( 'NONE',  ( -207.3438552930580272, 20.79694577641581077, -159.0697709843959728 ) ) ;
#10391=CARTESIAN_POINT ( 'NONE',  ( -207.1687172310330141, 20.08915143305816997, -158.9353507251184965 ) ) ;
#10400=CARTESIAN_POINT ( 'NONE',  ( 0.000000000000000000, 23.50000000000000000, 0.000000000000000000 ) ) ;
#10417=CARTESIAN_POINT ( 'NONE',  ( 226.6392846532197325, 19.96883746219288724, -130.8783844621844707 ) ) ;
#10449=CARTESIAN_POINT ( 'NONE',  ( 260.1353576186482996, 20.08915143297736705, -17.05322212017789951 ) ) ;
#10463=LINE ( 'NONE', #3583, #5519 ) ;
#10466=CARTESIAN_POINT ( 'NONE',  ( -130.8783844633512956, 19.96883746151126360, 226.6392846543344035 ) ) ;
#10490=CARTESIAN_POINT ( 'NONE',  ( -196.8887528224093444, 20.55460285074426707, 172.6991790975775132 ) ) ;
#10497=CARTESIAN_POINT ( 'NONE',  ( 178.3611219674585584, 20.79694577634646890, -190.4297758776777698 ) ) ;
#10516=CARTESIAN_POINT ( 'NONE',  ( 196.0019244007920349, 20.08915143297736705, -171.8850263962754354 ) ) ;
#10531=CARTESIAN_POINT ( 'NONE',  ( -196.7513681801157759, 19.96883745974439961, 172.5787240288376836 ) ) ;
#10534=CARTESIAN_POINT ( 'NONE',  ( -4.572608844893758122E-13, 20.79694577634647601, 260.7745447061711275 ) ) ;
#10536=CARTESIAN_POINT ( 'NONE',  ( -221.3800702329290857, 20.08915143297736350, 137.6665579279349174 ) ) ;
#10542=DIRECTION ( 'NONE',  ( 0.000000000000000000, 1.000000000000000000, 0.000000000000000000 ) ) ;
#10552=CARTESIAN_POINT ( 'NONE',  ( 84.14846197943569450, 19.96883746176665397, 247.8175805191055190 ) ) ;
#10555=DIRECTION ( 'NONE',  ( 1.200864985790633912E-16, -0.1961161351381850160, 0.9805806756909200006 ) ) ;
#10558=CARTESIAN_POINT ( 'NONE',  ( -252.0229195836992631, 20.79694577634646535, -67.53249125288884613 ) ) ;
#10560=CARTESIAN_POINT ( 'NONE',  ( 6.337788322448691496E-13, 20.79694577634647601, -260.7745447061711275 ) ) ;
#10565=ORIENTED_EDGE ( 'NONE', *, *, #1363, .T. ) ;
#10572=CARTESIAN_POINT ( 'NONE',  ( -251.0000000000000000, 24.99999999999995737, 0.000000000000000000 ) ) ;
#10589=CARTESIAN_POINT ( 'NONE',  ( 247.8175805195787689, 19.96883746176681740, 84.14846197955617413 ) ) ;
#10614=CARTESIAN_POINT ( 'NONE',  ( -34.20858920326337227, 20.55460285088512506, -259.6535381484778782 ) ) ;
#10618=CARTESIAN_POINT ( 'NONE',  ( -59.24444182677529369, 20.79694577634646890, 254.0989678903616777 ) ) ;
#10619=ORIENTED_EDGE ( 'NONE', *, *, #12408, .T. ) ;
#10635=DIRECTION ( 'NONE',  ( 1.000000000000000000, 0.000000000000000000, 0.000000000000000000 ) ) ;
#10655=CARTESIAN_POINT ( 'NONE',  ( 3.080812409053027094E-14, 24.75600756274008063, 251.5674242726970817 ) ) ;
#10657=CARTESIAN_POINT ( 'NONE',  ( -207.6469600138974272, 19.96883745988519365, -159.3024069661565534 ) ) ;
#10670=VERTEX_POINT ( 'NONE', #7363 ) ;
#10676=CARTESIAN_POINT ( 'NONE',  ( -1.010328782420808020E-12, 20.79694577634649022, 260.7745447061710138 ) ) ;
#10682=AXIS2_PLACEMENT_3D ( 'NONE', #11107, #5237, #9307 ) ;
#10697=CARTESIAN_POINT ( 'NONE',  ( -158.9353507255915190, 20.08915143292644245, -207.1687172315094756 ) ) ;
#10724=EDGE_CURVE ( 'NONE', #90, #1703, #2198, .T. ) ;
#10728=CARTESIAN_POINT ( 'NONE',  ( 34.18476129304277578, 19.96883745937039834, 259.4723857425807978 ) ) ;
#10745=CARTESIAN_POINT ( 'NONE',  ( -67.61424743051179576, 20.79694577629433283, 252.4341100433384781 ) ) ;
#10751=AXIS2_PLACEMENT_3D ( 'NONE', #5001, #9597, #7941 ) ;
#10756=CARTESIAN_POINT ( 'NONE',  ( 190.2689011420770271, 20.08915143297736705, 178.2104428091928696 ) ) ;
#10765=DIRECTION ( 'NONE',  ( 0.000000000000000000, 0.000000000000000000, 1.000000000000000000 ) ) ;
#10787=CARTESIAN_POINT ( 'NONE',  ( -84.20717312421410838, 20.55460285060721048, -247.9906035374705766 ) ) ;
#10808=CARTESIAN_POINT ( 'NONE',  ( -226.3083638773660198, 20.79694577627718388, -130.6873781515817825 ) ) ;
#10819=CARTESIAN_POINT ( 'NONE',  ( 91.83222442980259359, 20.08915143297736705, 243.9837273761028769 ) ) ;
#10823=CARTESIAN_POINT ( 'NONE',  ( -247.2466869553009872, 20.08915143298854389, 83.95474316008009907 ) ) ;
#10838=CIRCLE ( 'NONE', #6804, 246.0000000000000000 ) ;
#10854=CARTESIAN_POINT ( 'NONE',  ( 252.9796497720277841, 20.55460285096646089, 67.76049180220992696 ) ) ;
#10873=CARTESIAN_POINT ( 'NONE',  ( -115.4648407704221995, 20.08915143316778895, 234.1947771724274787 ) ) ;
#10875=CARTESIAN_POINT ( 'NONE',  ( 130.9697226060475259, 20.55460285142580545, -226.7975291077671329 ) ) ;
#10893=CARTESIAN_POINT ( 'NONE',  ( -258.8746690728235080, 20.08915143284549387, 34.10614053596890471 ) ) ;
#10905=PRESENTATION_STYLE_ASSIGNMENT (( #4829 ) ) ;
#10923=CARTESIAN_POINT ( 'NONE',  ( -196.8887528216966132, 20.55460285140358678, -172.6991790949711287 ) ) ;
#10929=CARTESIAN_POINT ( 'NONE',  ( -1.010328782420808020E-12, 20.79694577634649022, 260.7745447061710138 ) ) ;
#10946=CARTESIAN_POINT ( 'NONE',  ( -34.13493237016224668, 20.79694577639865471, 259.0935598599945138 ) ) ;
#10954=CIRCLE ( 'NONE', #12235, 3.000000000000002665 ) ;
#10981=CARTESIAN_POINT ( 'NONE',  ( -172.0303573358521305, 20.79694577634646535, -196.1676464792608954 ) ) ;
#10990=CARTESIAN_POINT ( 'NONE',  ( -130.9697226053157237, 20.55460285097016282, -226.7975291069864738 ) ) ;
#11017=PRODUCT_DEFINITION_CONTEXT ( 'detailed design', #1834, 'design' ) ;
#11022=CARTESIAN_POINT ( 'NONE',  ( -234.7354397754233446, 19.96883745989621417, -115.7315435906453871 ) ) ;
#11034=DIRECTION ( 'NONE',  ( 0.000000000000000000, -1.000000000000000000, 0.000000000000000000 ) ) ;
#11055=CARTESIAN_POINT ( 'NONE',  ( 226.7975291075301811, 20.55460285098495277, 130.9697226058104036 ) ) ;
#11074=CARTESIAN_POINT ( 'NONE',  ( 226.3083638779000069, 20.79694577591247295, -130.6873781523096056 ) ) ;
#11076=( BOUNDED_SURFACE ( )  B_SPLINE_SURFACE ( 3, 3, ( 
 ( #3739, #10008, #4935, #11877, #6816, #10873, #5813, #8277, #145, #10131, #4134, #1269, #4067, #6208, #6339, #10194, #11270, #10328, #2132, #12272, #5059, #10261, #5196, #10391, #6079, #9273, #4195, #1138, #8145, #12339, #11201, #12465, #12210, #2261, #3061, #3188, #12404, #1068, #5126, #7335, #8216, #2066, #11405, #9203, #2006, #80, #6139, #205, #7143, #7272, #3256, #8406, #5332, #9136, #7397, #3320, #9402, #269, #6277, #4327, #3122, #7201, #11336, #2200, #1205, #5264 ),
 ( #9334, #1003, #11, #4262, #8343, #9522, #10466, #11466, #9654, #10531, #4645, #12661, #3650, #1598, #11732, #3453, #2524, #6602, #3523, #4516, #1334, #4452, #536, #10657, #9712, #7592, #1463, #469, #2460, #12786, #7532, #11605, #8728, #11669, #1529, #5660, #2330, #594, #6475, #12528, #3587, #4584, #6406, #8537, #8660, #5594, #5401, #12718, #5527, #8601, #6536, #9468, #10589, #9585, #341, #7655, #2585, #4389, #8471, #3385, #1403, #7467, #6671, #10728, #11540, #12596 ),
 ( #2395, #5462, #402, #5928, #11858, #2648, #4712, #9992, #9855, #1798, #5561, #12857, #12055, #2843, #1728, #860, #664, #7722, #11997, #7995, #12990, #735, #9783, #1658, #10923, #6736, #11804, #10990, #2906, #10787, #3921, #8860, #3782, #4919, #4984, #1862, #6930, #8927, #6863, #11925, #12921, #5725, #8994, #9058, #2774, #3852, #7855, #4850, #8792, #5864, #6798, #10854, #3723, #7789, #11055, #4784, #2707, #6991, #1926, #9923, #794, #7921, #11306, #5997, #5794, #10055 ),
 ( #929, #12388, #8263, #4250, #7129, #2052, #3045, #4120, #12324, #11185, #1194, #8057, #8200, #5113, #8330, #7060, #12260, #5250, #6122, #2978, #3980, #2185, #10177, #10377, #5180, #9389, #7324, #3242, #9190, #3176, #7257, #9259, #10247, #11119, #990, #1991, #67, #6064, #10315, #11393, #1054, #2253, #3110, #7187, #11253, #2116, #193, #6327, #4051, #9320, #1254, #132, #6266, #8131, #12122, #5043, #5319, #6193, #1123, #10117, #9119, #202, #11322, #4182, #12191, #10929 ) ),
 .UNSPECIFIED., .F., .T., .F. ) 
 B_SPLINE_SURFACE_WITH_KNOTS ( ( 4, 4 ),
 ( 4, 2, 2, 2, 2, 2, 2, 2, 2, 2, 2, 2, 2, 2, 2, 2, 2, 2, 2, 2, 2, 2, 2, 2, 2, 2, 2, 2, 2, 2, 2, 2, 4 ),
 ( 0.000000000000000000, 1.000000000000000000 ),
 ( 0.5000000000000000000, 0.5312500000000000000, 0.5625000000000000000, 0.5937500000000000000, 0.6250000000000000000, 0.6562500000000000000, 0.6875000000000000000, 0.7187500000000000000, 0.7500000000000000000, 0.7812500000000000000, 0.8125000000000000000, 0.8437500000000000000, 0.8750000000000000000, 0.9062500000000000000, 0.9375000000000000000, 0.9687500000000000000, 1.000000000000000000, 1.031250000000000000, 1.062500000000000000, 1.093750000000000000, 1.125000000000000000, 1.156250000000000000, 1.187500000000000000, 1.218750000000000000, 1.250000000000000000, 1.281250000000000000, 1.312500000000000000, 1.343750000000000000, 1.375000000000000000, 1.406250000000000000, 1.437500000000000000, 1.468750000000000000, 1.500000000000000000 ),
 .UNSPECIFIED. ) 
 GEOMETRIC_REPRESENTATION_ITEM ( )  RATIONAL_B_SPLINE_SURFACE ( (
 ( 1.000000000000000000, 1.000000000000000000, 1.000000000000000000, 1.000000000000000000, 1.000000000000000000, 1.000000000000000000, 1.000000000000000000, 1.000000000000000000, 1.000000000000000000, 1.000000000000000000, 1.000000000000000000, 1.000000000000000000, 1.000000000000000000, 1.000000000000000000, 1.000000000000000000, 1.000000000000000000, 1.000000000000000000, 1.000000000000000000, 1.000000000000000000, 1.000000000000000000, 1.000000000000000000, 1.000000000000000000, 1.000000000000000000, 1.000000000000000000, 1.000000000000000000, 1.000000000000000000, 1.000000000000000000, 1.000000000000000000, 1.000000000000000000, 1.000000000000000000, 1.000000000000000000, 1.000000000000000000, 1.000000000000000000, 1.000000000000000000, 1.000000000000000000, 1.000000000000000000, 1.000000000000000000, 1.000000000000000000, 1.000000000000000000, 1.000000000000000000, 1.000000000000000000, 1.000000000000000000, 1.000000000000000000, 1.000000000000000000, 1.000000000000000000, 1.000000000000000000, 1.000000000000000000, 1.000000000000000000, 1.000000000000000000, 1.000000000000000000, 1.000000000000000000, 1.000000000000000000, 1.000000000000000000, 1.000000000000000000, 1.000000000000000000, 1.000000000000000000, 1.000000000000000000, 1.000000000000000000, 1.000000000000000000, 1.000000000000000000, 1.000000000000000000, 1.000000000000000000, 1.000000000000000000, 1.000000000000000000, 1.000000000000000000, 1.000000000000000000),
 ( 0.4027746460044325238, 0.4027746460044325238, 0.4027746460044540067, 0.4027746460044540067, 0.4027746460044225318, 0.4027746460044225318, 0.4027746460043825083, 0.4027746460043825083, 0.4027746460043430399, 0.4027746460043430399, 0.4027746460043289956, 0.4027746460043289956, 0.4027746460043410415, 0.4027746460043410415, 0.4027746460044525079, 0.4027746460044525079, 0.4027746460044325238, 0.4027746460044325238, 0.4027746460044525079, 0.4027746460044525079, 0.4027746460043595267, 0.4027746460043595267, 0.4027746460044215326, 0.4027746460044215326, 0.4027746460043590271, 0.4027746460043590271, 0.4027746460044335230, 0.4027746460044335230, 0.4027746460043410415, 0.4027746460043410415, 0.4027746460042145316, 0.4027746460042145316, 0.4027746460044325238, 0.4027746460044325238, 0.4027746460044535071, 0.4027746460044535071, 0.4027746460044230314, 0.4027746460044230314, 0.4027746460043575283, 0.4027746460043575283, 0.4027746460043590271, 0.4027746460043590271, 0.4027746460043944987, 0.4027746460043944987, 0.4027746460043630239, 0.4027746460043630239, 0.4027746460044520083, 0.4027746460044520083, 0.4027746460044325238, 0.4027746460044325238, 0.4027746460044530075, 0.4027746460044530075, 0.4027746460043180043, 0.4027746460043180043, 0.4027746460043225007, 0.4027746460043225007, 0.4027746460043230003, 0.4027746460043230003, 0.4027746460043944987, 0.4027746460043944987, 0.4027746460042090360, 0.4027746460042090360, 0.4027746460044520083, 0.4027746460044520083, 0.4027746460044325238, 0.4027746460044325238),
 ( 0.4027746460044325238, 0.4027746460044325238, 0.4027746460044540067, 0.4027746460044540067, 0.4027746460044225318, 0.4027746460044225318, 0.4027746460043825083, 0.4027746460043825083, 0.4027746460043430399, 0.4027746460043430399, 0.4027746460043289956, 0.4027746460043289956, 0.4027746460043410415, 0.4027746460043410415, 0.4027746460044525079, 0.4027746460044525079, 0.4027746460044325238, 0.4027746460044325238, 0.4027746460044525079, 0.4027746460044525079, 0.4027746460043595267, 0.4027746460043595267, 0.4027746460044215326, 0.4027746460044215326, 0.4027746460043590271, 0.4027746460043590271, 0.4027746460044335230, 0.4027746460044335230, 0.4027746460043410415, 0.4027746460043410415, 0.4027746460042145316, 0.4027746460042145316, 0.4027746460044325238, 0.4027746460044325238, 0.4027746460044535071, 0.4027746460044535071, 0.4027746460044230314, 0.4027746460044230314, 0.4027746460043575283, 0.4027746460043575283, 0.4027746460043590271, 0.4027746460043590271, 0.4027746460043944987, 0.4027746460043944987, 0.4027746460043630239, 0.4027746460043630239, 0.4027746460044520083, 0.4027746460044520083, 0.4027746460044325238, 0.4027746460044325238, 0.4027746460044530075, 0.4027746460044530075, 0.4027746460043180043, 0.4027746460043180043, 0.4027746460043225007, 0.4027746460043225007, 0.4027746460043230003, 0.4027746460043230003, 0.4027746460043944987, 0.4027746460043944987, 0.4027746460042090360, 0.4027746460042090360, 0.4027746460044520083, 0.4027746460044520083, 0.4027746460044325238, 0.4027746460044325238),
 ( 1.000000000000000000, 1.000000000000000000, 1.000000000000000000, 1.000000000000000000, 1.000000000000000000, 1.000000000000000000, 1.000000000000000000, 1.000000000000000000, 1.000000000000000000, 1.000000000000000000, 1.000000000000000000, 1.000000000000000000, 1.000000000000000000, 1.000000000000000000, 1.000000000000000000, 1.000000000000000000, 1.000000000000000000, 1.000000000000000000, 1.000000000000000000, 1.000000000000000000, 1.000000000000000000, 1.000000000000000000, 1.000000000000000000, 1.000000000000000000, 1.000000000000000000, 1.000000000000000000, 1.000000000000000000, 1.000000000000000000, 1.000000000000000000, 1.000000000000000000, 1.000000000000000000, 1.000000000000000000, 1.000000000000000000, 1.000000000000000000, 1.000000000000000000, 1.000000000000000000, 1.000000000000000000, 1.000000000000000000, 1.000000000000000000, 1.000000000000000000, 1.000000000000000000, 1.000000000000000000, 1.000000000000000000, 1.000000000000000000, 1.000000000000000000, 1.000000000000000000, 1.000000000000000000, 1.000000000000000000, 1.000000000000000000, 1.000000000000000000, 1.000000000000000000, 1.000000000000000000, 1.000000000000000000, 1.000000000000000000, 1.000000000000000000, 1.000000000000000000, 1.000000000000000000, 1.000000000000000000, 1.000000000000000000, 1.000000000000000000, 1.000000000000000000, 1.000000000000000000, 1.000000000000000000, 1.000000000000000000, 1.000000000000000000, 1.000000000000000000) ) ) 
 REPRESENTATION_ITEM ( '' )  SURFACE ( )  );
#11079=DIRECTION ( 'NONE',  ( 1.125045280045195686E-16, -0.3950277506594045973, 0.9186691875800402363 ) ) ;
#11091=CARTESIAN_POINT ( 'NONE',  ( 17.05314194195614874, 20.08915143307225648, 260.5542428346390125 ) ) ;
#11097=AXIS2_PLACEMENT_3D ( 'NONE', #9041, #174, #12102 ) ;
#11107=CARTESIAN_POINT ( 'NONE',  ( 0.000000000000000000, 24.99999999999995737, 0.000000000000000000 ) ) ;
#11119=CARTESIAN_POINT ( 'NONE',  ( 17.06760680800665142, 20.79694577634646180, -260.7745447061710138 ) ) ;
#11132=AXIS2_PLACEMENT_3D ( 'NONE', #3068, #7079, #10202 ) ;
#11158=CARTESIAN_POINT ( 'NONE',  ( -261.1558126970361400, 19.96883746053716990, -17.09264059830048410 ) ) ;
#11163=CARTESIAN_POINT ( 'NONE',  ( 8.533827019709789852, 20.79694577634646180, 260.7745447061712412 ) ) ;
#11170=CARTESIAN_POINT ( 'NONE',  ( 0.000000000000000000, 22.00000000000000000, 0.000000000000000000 ) ) ;
#11174=CARTESIAN_POINT ( 'NONE',  ( 3.066299324940445530E-14, 21.99999999999995381, 250.3823410207189966 ) ) ;
#11176=CARTESIAN_POINT ( 'NONE',  ( -17.06764083276507904, 20.79694577634647601, 260.3553053170168141 ) ) ;
#11185=CARTESIAN_POINT ( 'NONE',  ( -196.4640694352650030, 20.79694577634417030, 172.3268284098779759 ) ) ;
#11201=CARTESIAN_POINT ( 'NONE',  ( -67.55708173894439028, 20.08915143292001204, -252.2208631666825056 ) ) ;
#11213=DIRECTION ( 'NONE',  ( 0.000000000000000000, 0.000000000000000000, -1.000000000000000000 ) ) ;
#11220=CARTESIAN_POINT ( 'NONE',  ( -67.71318189681706201, 19.96883746180772690, 252.8031682256479655 ) ) ;
#11225=CARTESIAN_POINT ( 'NONE',  ( 34.05310945291965652, 20.79694577634646180, 258.6823826759384133 ) ) ;
#11246=CARTESIAN_POINT ( 'NONE',  ( 6.345753394971347358E-13, 20.08915143297736350, -260.5542428351130866 ) ) ;
#11253=CARTESIAN_POINT ( 'NONE',  ( 234.3927740976959910, 20.79694577647348908, -115.5625104414818054 ) ) ;
#11270=CARTESIAN_POINT ( 'NONE',  ( -260.5542428346390125, 20.08915143307225648, 17.05314194216809653 ) ) ;
#11290=CARTESIAN_POINT ( 'NONE',  ( -17.09264059776470290, 19.96883746054087538, 261.1558126970361400 ) ) ;
#11300=CIRCLE ( 'NONE', #7260, 246.0000000000000000 ) ;
#11306=CARTESIAN_POINT ( 'NONE',  ( 67.76049180374880621, 20.55460285150727273, 252.9796497720274147 ) ) ;
#11307=( NAMED_UNIT ( * ) SI_UNIT ( $, .STERADIAN. ) SOLID_ANGLE_UNIT ( ) );
#11318=LINE ( 'NONE', #1190, #190 ) ;
#11322=CARTESIAN_POINT ( 'NONE',  ( 67.61424743078299571, 20.79694577590440119, 252.4341100442090067 ) ) ;
#11336=CARTESIAN_POINT ( 'NONE',  ( 67.55708173931988370, 20.08915143256180968, 252.2208631684339935 ) ) ;
#11345=AXIS2_PLACEMENT_3D ( 'NONE', #10400, #8286, #9410 ) ;
#11360=CARTESIAN_POINT ( 'NONE',  ( -172.6991790963936921, 20.55460285138878618, 196.8887528212225106 ) ) ;
#11386=CARTESIAN_POINT ( 'NONE',  ( -4.572608844893758122E-13, 20.79694577634647601, 260.7745447061711275 ) ) ;
#11393=CARTESIAN_POINT ( 'NONE',  ( 159.0697709852749995, 20.79694577591498472, -207.3438552938715134 ) ) ;
#11403=EDGE_LOOP ( 'NONE', ( #12223, #7140 ) ) ;
#11405=CARTESIAN_POINT ( 'NONE',  ( 207.1687172302655142, 20.08915143321463503, -158.9353507248590063 ) ) ;
#11424=CARTESIAN_POINT ( 'NONE',  ( -261.3381329044966606, 20.55460285096646089, -17.10461161606123426 ) ) ;
#11466=CARTESIAN_POINT ( 'NONE',  ( -159.3024069656823940, 19.96883745967399548, 207.6469600131863729 ) ) ;
#11490=CARTESIAN_POINT ( 'NONE',  ( -84.20717312374198116, 20.55460285077014504, 247.9906035358103225 ) ) ;
#11523=CARTESIAN_POINT ( 'NONE',  ( 158.7026972336036579, 20.08915143297736705, -206.8203823583188807 ) ) ;
#11533=TOROIDAL_SURFACE ( 'NONE', #9572, 250.3823410207189966, 3.000000000000000000 ) ;
#11540=CARTESIAN_POINT ( 'NONE',  ( 17.09264059776268851, 19.96883746064459331, 261.1558126970361400 ) ) ;
#11559=CARTESIAN_POINT ( 'NONE',  ( 130.8783844628973441, 19.96883745980737501, -226.6392846544037809 ) ) ;
#11564=CARTESIAN_POINT ( 'NONE',  ( -254.0989678903619051, 20.79694577634646535, 59.24444182677424919 ) ) ;
#11566=CARTESIAN_POINT ( 'NONE',  ( 225.9597979674045405, 20.79694577634646535, -130.4544329367267324 ) ) ;
#11598=SHAPE_DEFINITION_REPRESENTATION ( #6794, #8443 ) ;
#11605=CARTESIAN_POINT ( 'NONE',  ( -34.18476129325013346, 19.96883746093702428, -259.4723857429224267 ) ) ;
#11610=CARTESIAN_POINT ( 'NONE',  ( -246.8597181602070236, 20.08915143297737060, -83.79436865282342239 ) ) ;
#11624=CARTESIAN_POINT ( 'NONE',  ( -115.8123742913374770, 20.55460285152583921, -234.8993005728878529 ) ) ;
#11630=CARTESIAN_POINT ( 'NONE',  ( -247.0684411393755795, 20.79694577634646535, -83.86521783953202203 ) ) ;
#11634=CARTESIAN_POINT ( 'NONE',  ( 17.06764083276477706, 20.79694577634646890, -260.3553053170167004 ) ) ;
#11669=CARTESIAN_POINT ( 'NONE',  ( 17.09264059789564172, 19.96883746058902176, -261.1558126970361400 ) ) ;
#11674=CARTESIAN_POINT ( 'NONE',  ( -237.4577367525706393, 20.08915143297736705, 107.5873595010535411 ) ) ;
#11691=CARTESIAN_POINT ( 'NONE',  ( -84.02568524183371323, 20.79694577604410100, 247.4557548106605225 ) ) ;
#11699=CIRCLE ( 'NONE', #453, 250.7029414592220178 ) ;
#11708=CARTESIAN_POINT ( 'NONE',  ( -226.1171533167550081, 20.08915143289658545, -130.5770120871825952 ) ) ;
#11713=EDGE_LOOP ( 'NONE', ( #5989, #2643 ) ) ;
#11732=CARTESIAN_POINT ( 'NONE',  ( -252.8031682270705289, 19.96883745940372279, 67.71318189758537187 ) ) ;
#11752=ADVANCED_BREP_SHAPE_REPRESENTATION ( '', ( #1525, #805 ), #391 ) ;
#11754=CARTESIAN_POINT ( 'NONE',  ( 34.20858920311310669, 20.55460285062568815, 259.6535381495587558 ) ) ;
#11766=CARTESIAN_POINT ( 'NONE',  ( 225.7689075324037162, 20.08915143297736705, 130.3442252640563481 ) ) ;
#11773=CARTESIAN_POINT ( 'NONE',  ( 115.4648407707963997, 20.08915143305429041, -234.1947771728865177 ) ) ;
#11780=ORIENTED_EDGE ( 'NONE', *, *, #8186, .T. ) ;
#11804=CARTESIAN_POINT ( 'NONE',  ( -159.4136521839998011, 20.55460285116278385, -207.7919029849606432 ) ) ;
#11822=CARTESIAN_POINT ( 'NONE',  ( 115.8123742910162264, 20.55460285096275541, -234.8993005738286115 ) ) ;
#11831=EDGE_LOOP ( 'NONE', ( #9164, #4582, #5092, #3076 ) ) ;
#11833=CARTESIAN_POINT ( 'NONE',  ( 42.46883004693734875, 20.08915143297736350, 257.2112267038639288 ) ) ;
#11837=CARTESIAN_POINT ( 'NONE',  ( -247.2466869557850089, 20.08915143288961858, -83.95474316020511196 ) ) ;
#11847=EDGE_CURVE ( 'NONE', #10670, #9039, #10838, .T. ) ;
#11858=CARTESIAN_POINT ( 'NONE',  ( -84.20717312374198116, 20.55460285077014504, 247.9906035358103225 ) ) ;
#11862=EDGE_CURVE ( 'NONE', #3549, #8633, #11699, .T. ) ;
#11877=CARTESIAN_POINT ( 'NONE',  ( -67.55708173888510260, 20.08915143292433214, 252.2208631666720180 ) ) ;
#11879=CARTESIAN_POINT ( 'NONE',  ( 261.3381329044966606, 20.55460285106647689, 17.10461161501256555 ) ) ;
#11894=CARTESIAN_POINT ( 'NONE',  ( -172.1812796679919870, 20.08915143287683591, 196.2980642839890209 ) ) ;
#11902=EDGE_LOOP ( 'NONE', ( #942, #4478, #6306, #4551 ) ) ;
#11904=EDGE_LOOP ( 'NONE', ( #2164, #10340, #10565, #2284 ) ) ;
#11907=DIRECTION ( 'NONE',  ( 0.000000000000000000, 1.000000000000000000, 0.000000000000000000 ) ) ;
#11914=CARTESIAN_POINT ( 'NONE',  ( -83.86521783953165254, 20.79694577634646535, -247.0684411393756363 ) ) ;
#11924=ORIENTED_EDGE ( 'NONE', *, *, #12335, .T. ) ;
#11925=CARTESIAN_POINT ( 'NONE',  ( 159.4136521832723474, 20.55460285070720161, -207.7919029841772840 ) ) ;
#11947=CARTESIAN_POINT ( 'NONE',  ( -130.6873781513712061, 20.79694577639645203, -226.3083638771730079 ) ) ;
#11965=( LENGTH_UNIT ( ) NAMED_UNIT ( * ) SI_UNIT ( .MILLI., .METRE. ) );
#11984=CARTESIAN_POINT ( 'NONE',  ( -151.9741924115230347, 20.79694577634646535, -212.0849693193239602 ) ) ;
#11994=ORIENTED_EDGE ( 'NONE', *, *, #7506, .F. ) ;
#11997=CARTESIAN_POINT ( 'NONE',  ( -259.6535381484769118, 20.55460285079236016, -34.20858920326526942 ) ) ;
#12016=CARTESIAN_POINT ( 'NONE',  ( 130.6873781525580114, 20.79694577610125705, 226.3083638772055224 ) ) ;
#12031=CARTESIAN_POINT ( 'NONE',  ( -34.18476129325013346, 19.96883746093702428, -259.4723857429224267 ) ) ;
#12035=DIRECTION ( 'NONE',  ( 0.000000000000000000, 0.000000000000000000, -1.000000000000000000 ) ) ;
#12055=CARTESIAN_POINT ( 'NONE',  ( -234.8993005728878529, 20.55460285095910677, 115.8123742916932741 ) ) ;
#12068=ORIENTED_EDGE ( 'NONE', *, *, #4393, .F. ) ;
#12073=CARTESIAN_POINT ( 'NONE',  ( 159.0697709834164755, 20.79694577659177313, 207.3438552932204857 ) ) ;
#12082=ORIENTED_EDGE ( 'NONE', *, *, #6243, .F. ) ;
#12091=CARTESIAN_POINT ( 'NONE',  ( 247.2466869557899827, 20.08915143289970473, -83.95474316006121285 ) ) ;
#12092=DIRECTION ( 'NONE',  ( 0.000000000000000000, 0.000000000000000000, -1.000000000000000000 ) ) ;
#12095=CARTESIAN_POINT ( 'NONE',  ( 0.000000000000000000, 24.99999999999995737, 0.000000000000000000 ) ) ;
#12102=DIRECTION ( 'NONE',  ( 0.000000000000000000, 0.000000000000000000, 1.000000000000000000 ) ) ;
#12109=CARTESIAN_POINT ( 'NONE',  ( -34.02434144668546168, 20.08915143297736705, -258.4638482596386098 ) ) ;
#12113=CARTESIAN_POINT ( 'NONE',  ( -42.50473797389721398, 20.79694577634646535, -257.4287020129719963 ) ) ;
#12122=CARTESIAN_POINT ( 'NONE',  ( 226.3083638770190191, 20.79694577655596888, 130.6873781509345918 ) ) ;
#12138=ADVANCED_FACE ( 'NONE', ( #8636 ), #12984, .F. ) ;
#12158=CARTESIAN_POINT ( 'NONE',  ( 67.55708173931988370, 20.08915143256180968, 252.2208631684339935 ) ) ;
#12174=CARTESIAN_POINT ( 'NONE',  ( -190.2689011420770271, 20.08915143297736705, -178.2104428091929549 ) ) ;
#12188=CARTESIAN_POINT ( 'NONE',  ( 34.02434144668578853, 20.08915143297736350, -258.4638482596385529 ) ) ;
#12191=CARTESIAN_POINT ( 'NONE',  ( 17.06760680892275062, 20.79694577654979071, 260.7745447056980197 ) ) ;
#12210=CARTESIAN_POINT ( 'NONE',  ( -17.05314194221659818, 20.08915143297737416, -260.5542428351129729 ) ) ;
#12222=CARTESIAN_POINT ( 'NONE',  ( 0.000000000000000000, 23.50000000000000000, 0.000000000000000000 ) ) ;
#12223=ORIENTED_EDGE ( 'NONE', *, *, #2684, .T. ) ;
#12228=CARTESIAN_POINT ( 'NONE',  ( 252.2208631679629889, 20.08915143265645042, -67.55708173926119287 ) ) ;
#12235=AXIS2_PLACEMENT_3D ( 'NONE', #11174, #5100, #6181 ) ;
#12246=CARTESIAN_POINT ( 'NONE',  ( -171.8850263962752649, 20.08915143297736350, -196.0019244007921486 ) ) ;
#12251=PLANE ( 'NONE',  #8385 ) ;
#12260=CARTESIAN_POINT ( 'NONE',  ( -260.7745447056980197, 20.79694577654979071, 17.06760680913495065 ) ) ;
#12272=CARTESIAN_POINT ( 'NONE',  ( -252.2208631662124958, 20.08915143301432948, -67.55708173888800161 ) ) ;
#12277=CARTESIAN_POINT ( 'NONE',  ( 207.3438552925264844, 20.79694577678052880, -159.0697709836649949 ) ) ;
#12289=CARTESIAN_POINT ( 'NONE',  ( 34.10614053541959834, 20.08915143339292442, 258.8746690701424882 ) ) ;
#12295=CARTESIAN_POINT ( 'NONE',  ( 130.4544329367266471, 20.79694577634646180, 225.9597979674046542 ) ) ;
#12307=CARTESIAN_POINT ( 'NONE',  ( -17.05322212017792793, 20.08915143297736705, -260.1353576186481860 ) ) ;
#12324=CARTESIAN_POINT ( 'NONE',  ( -172.3268284098719789, 20.79694577634883856, 196.4640694352564765 ) ) ;
#12335=EDGE_CURVE ( 'NONE', #12702, #9039, #1141, .T. ) ;
#12339=CARTESIAN_POINT ( 'NONE',  ( -83.95474316008289861, 20.08915143298712280, -247.2466869553079789 ) ) ;
#12350=ORIENTED_EDGE ( 'NONE', *, *, #8077, .T. ) ;
#12360=CARTESIAN_POINT ( 'NONE',  ( 34.18476129304277578, 19.96883745937039834, 259.4723857425807978 ) ) ;
#12388=CARTESIAN_POINT ( 'NONE',  ( -17.06760680892479698, 20.79694577614318973, 260.7745447066434963 ) ) ;
#12404=CARTESIAN_POINT ( 'NONE',  ( 83.95474316006190918, 20.08915143290042948, -247.2466869557860036 ) ) ;
#12408=EDGE_CURVE ( 'NONE', #6668, #3483, #5628, .T. ) ;
#12427=CARTESIAN_POINT ( 'NONE',  ( -67.76049180241520276, 20.55460285097757378, 252.9796497716870078 ) ) ;
#12432=CARTESIAN_POINT ( 'NONE',  ( 244.1900186690936039, 20.79694577634646890, 91.90986972409962164 ) ) ;
#12447=( BOUNDED_SURFACE ( )  B_SPLINE_SURFACE ( 3, 3, ( 
 ( #4891, #12894, #3891, #1835, #6902, #7762, #2743, #6832, #11894, #4754, #770, #5897, #4817, #10823, #8964, #10893, #5766, #705, #8830, #13025, #11837, #1768, #11708, #8895, #12958, #6641, #10697, #1572, #6708, #12759, #8763, #3824, #1630, #9690, #4616, #8693, #7694, #11773, #2621, #12827, #10090, #1160, #5217, #2949, #9291, #12091, #12228, #6035, #7910, #4152, #7029, #2025, #963, #5020, #9092, #1896, #1022, #6097, #2882, #2788, #7230, #10024, #12158, #12289, #11091, #4020 ),
 ( #8098, #11290, #3956, #11220, #9157, #10284, #6964, #8167, #2152, #3012, #1960, #10148, #3143, #30, #7095, #5082, #9031, #11158, #4087, #3081, #896, #11022, #6232, #7161, #8029, #162, #7965, #2085, #6162, #10217, #1089, #12031, #5147, #5968, #99, #9227, #8235, #4955, #11559, #6299, #5283, #296, #2417, #10417, #3276, #3478, #4352, #10348, #3210, #1484, #7358, #2221, #3338, #12614, #6496, #7417, #8300, #6557, #5356, #423, #5423, #10552, #8363, #12360, #1222, #1421 ),
 ( #2280, #9359, #4472, #12427, #11490, #6360, #1292, #9427, #11360, #10490, #2353, #7293, #8429, #7553, #225, #12484, #8555, #11424, #6426, #12549, #1358, #9487, #4283, #8492, #358, #4406, #3405, #7488, #11624, #5480, #2478, #10614, #9603, #9540, #5547, #4215, #2544, #11822, #10875, #8677, #12739, #5818, #6692, #556, #9879, #3608, #491, #7676, #4601, #11879, #6622, #12808, #1749, #6883, #12939, #3540, #2666, #7612, #4736, #7875, #6755, #756, #4804, #11754, #2605, #617 ),
 ( #10676, #12681, #10946, #10745, #11691, #3674, #8876, #7805, #7747, #4539, #2796, #1616, #5680, #1681, #1817, #9732, #1550, #8815, #4668, #3807, #8747, #5615, #10808, #9673, #5748, #9804, #5885, #11947, #8622, #684, #3741, #12877, #2727, #6819, #6949, #13010, #1943, #3873, #3067, #5132, #9194, #9208, #12277, #11074, #811, #9938, #6145, #10201, #10010, #2069, #5064, #3939, #7147, #2864, #2138, #1007, #1073, #2011, #12073, #12016, #7945, #4285, #8949, #4873, #17, #85 ) ),
 .UNSPECIFIED., .F., .T., .T. ) 
 B_SPLINE_SURFACE_WITH_KNOTS ( ( 4, 4 ),
 ( 4, 2, 2, 2, 2, 2, 2, 2, 2, 2, 2, 2, 2, 2, 2, 2, 2, 2, 2, 2, 2, 2, 2, 2, 2, 2, 2, 2, 2, 2, 2, 2, 4 ),
 ( 0.000000000000000000, 1.000000000000000000 ),
 ( 0.5000000000000000000, 0.5312500000000000000, 0.5625000000000000000, 0.5937500000000000000, 0.6250000000000000000, 0.6562500000000000000, 0.6875000000000000000, 0.7187500000000000000, 0.7500000000000000000, 0.7812500000000000000, 0.8125000000000000000, 0.8437500000000000000, 0.8750000000000000000, 0.9062500000000000000, 0.9375000000000000000, 0.9687500000000000000, 1.000000000000000000, 1.031250000000000000, 1.062500000000000000, 1.093750000000000000, 1.125000000000000000, 1.156250000000000000, 1.187500000000000000, 1.218750000000000000, 1.250000000000000000, 1.281250000000000000, 1.312500000000000000, 1.343750000000000000, 1.375000000000000000, 1.406250000000000000, 1.437500000000000000, 1.468750000000000000, 1.500000000000000000 ),
 .UNSPECIFIED. ) 
 GEOMETRIC_REPRESENTATION_ITEM ( )  RATIONAL_B_SPLINE_SURFACE ( (
 ( 1.000000000000000000, 1.000000000000000000, 1.000000000000000000, 1.000000000000000000, 1.000000000000000000, 1.000000000000000000, 1.000000000000000000, 1.000000000000000000, 1.000000000000000000, 1.000000000000000000, 1.000000000000000000, 1.000000000000000000, 1.000000000000000000, 1.000000000000000000, 1.000000000000000000, 1.000000000000000000, 1.000000000000000000, 1.000000000000000000, 1.000000000000000000, 1.000000000000000000, 1.000000000000000000, 1.000000000000000000, 1.000000000000000000, 1.000000000000000000, 1.000000000000000000, 1.000000000000000000, 1.000000000000000000, 1.000000000000000000, 1.000000000000000000, 1.000000000000000000, 1.000000000000000000, 1.000000000000000000, 1.000000000000000000, 1.000000000000000000, 1.000000000000000000, 1.000000000000000000, 1.000000000000000000, 1.000000000000000000, 1.000000000000000000, 1.000000000000000000, 1.000000000000000000, 1.000000000000000000, 1.000000000000000000, 1.000000000000000000, 1.000000000000000000, 1.000000000000000000, 1.000000000000000000, 1.000000000000000000, 1.000000000000000000, 1.000000000000000000, 1.000000000000000000, 1.000000000000000000, 1.000000000000000000, 1.000000000000000000, 1.000000000000000000, 1.000000000000000000, 1.000000000000000000, 1.000000000000000000, 1.000000000000000000, 1.000000000000000000, 1.000000000000000000, 1.000000000000000000, 1.000000000000000000, 1.000000000000000000, 1.000000000000000000, 1.000000000000000000),
 ( 0.4027746460044325238, 0.4027746460044325238, 0.4027746460044540067, 0.4027746460044540067, 0.4027746460044225318, 0.4027746460044225318, 0.4027746460043825083, 0.4027746460043825083, 0.4027746460043430399, 0.4027746460043430399, 0.4027746460043289956, 0.4027746460043289956, 0.4027746460043410415, 0.4027746460043410415, 0.4027746460044525079, 0.4027746460044525079, 0.4027746460044325238, 0.4027746460044325238, 0.4027746460044525079, 0.4027746460044525079, 0.4027746460043595267, 0.4027746460043595267, 0.4027746460044215326, 0.4027746460044215326, 0.4027746460043590271, 0.4027746460043590271, 0.4027746460044335230, 0.4027746460044335230, 0.4027746460043410415, 0.4027746460043410415, 0.4027746460042145316, 0.4027746460042145316, 0.4027746460044325238, 0.4027746460044325238, 0.4027746460044535071, 0.4027746460044535071, 0.4027746460044230314, 0.4027746460044230314, 0.4027746460043575283, 0.4027746460043575283, 0.4027746460043590271, 0.4027746460043590271, 0.4027746460043944987, 0.4027746460043944987, 0.4027746460043630239, 0.4027746460043630239, 0.4027746460044520083, 0.4027746460044520083, 0.4027746460044325238, 0.4027746460044325238, 0.4027746460044530075, 0.4027746460044530075, 0.4027746460043180043, 0.4027746460043180043, 0.4027746460043225007, 0.4027746460043225007, 0.4027746460043230003, 0.4027746460043230003, 0.4027746460043944987, 0.4027746460043944987, 0.4027746460042090360, 0.4027746460042090360, 0.4027746460044520083, 0.4027746460044520083, 0.4027746460044325238, 0.4027746460044325238),
 ( 0.4027746460044325238, 0.4027746460044325238, 0.4027746460044540067, 0.4027746460044540067, 0.4027746460044225318, 0.4027746460044225318, 0.4027746460043825083, 0.4027746460043825083, 0.4027746460043430399, 0.4027746460043430399, 0.4027746460043289956, 0.4027746460043289956, 0.4027746460043410415, 0.4027746460043410415, 0.4027746460044525079, 0.4027746460044525079, 0.4027746460044325238, 0.4027746460044325238, 0.4027746460044525079, 0.4027746460044525079, 0.4027746460043595267, 0.4027746460043595267, 0.4027746460044215326, 0.4027746460044215326, 0.4027746460043590271, 0.4027746460043590271, 0.4027746460044335230, 0.4027746460044335230, 0.4027746460043410415, 0.4027746460043410415, 0.4027746460042145316, 0.4027746460042145316, 0.4027746460044325238, 0.4027746460044325238, 0.4027746460044535071, 0.4027746460044535071, 0.4027746460044230314, 0.4027746460044230314, 0.4027746460043575283, 0.4027746460043575283, 0.4027746460043590271, 0.4027746460043590271, 0.4027746460043944987, 0.4027746460043944987, 0.4027746460043630239, 0.4027746460043630239, 0.4027746460044520083, 0.4027746460044520083, 0.4027746460044325238, 0.4027746460044325238, 0.4027746460044530075, 0.4027746460044530075, 0.4027746460043180043, 0.4027746460043180043, 0.4027746460043225007, 0.4027746460043225007, 0.4027746460043230003, 0.4027746460043230003, 0.4027746460043944987, 0.4027746460043944987, 0.4027746460042090360, 0.4027746460042090360, 0.4027746460044520083, 0.4027746460044520083, 0.4027746460044325238, 0.4027746460044325238),
 ( 1.000000000000000000, 1.000000000000000000, 1.000000000000000000, 1.000000000000000000, 1.000000000000000000, 1.000000000000000000, 1.000000000000000000, 1.000000000000000000, 1.000000000000000000, 1.000000000000000000, 1.000000000000000000, 1.000000000000000000, 1.000000000000000000, 1.000000000000000000, 1.000000000000000000, 1.000000000000000000, 1.000000000000000000, 1.000000000000000000, 1.000000000000000000, 1.000000000000000000, 1.000000000000000000, 1.000000000000000000, 1.000000000000000000, 1.000000000000000000, 1.000000000000000000, 1.000000000000000000, 1.000000000000000000, 1.000000000000000000, 1.000000000000000000, 1.000000000000000000, 1.000000000000000000, 1.000000000000000000, 1.000000000000000000, 1.000000000000000000, 1.000000000000000000, 1.000000000000000000, 1.000000000000000000, 1.000000000000000000, 1.000000000000000000, 1.000000000000000000, 1.000000000000000000, 1.000000000000000000, 1.000000000000000000, 1.000000000000000000, 1.000000000000000000, 1.000000000000000000, 1.000000000000000000, 1.000000000000000000, 1.000000000000000000, 1.000000000000000000, 1.000000000000000000, 1.000000000000000000, 1.000000000000000000, 1.000000000000000000, 1.000000000000000000, 1.000000000000000000, 1.000000000000000000, 1.000000000000000000, 1.000000000000000000, 1.000000000000000000, 1.000000000000000000, 1.000000000000000000, 1.000000000000000000, 1.000000000000000000, 1.000000000000000000, 1.000000000000000000) ) ) 
 REPRESENTATION_ITEM ( '' )  SURFACE ( )  );
#12454=CARTESIAN_POINT ( 'NONE',  ( 206.8203823583192502, 20.08915143297736705, 158.7026972336032600 ) ) ;
#12465=CARTESIAN_POINT ( 'NONE',  ( -34.10614053579494964, 20.08915143303473982, -258.8746690718934929 ) ) ;
#12484=CARTESIAN_POINT ( 'NONE',  ( -259.6535381480032356, 20.55460285108499008, 34.20858920320377905 ) ) ;
#12489=CARTESIAN_POINT ( 'NONE',  ( -158.8368823490027921, 20.79694577634646535, 206.9952515782965179 ) ) ;
#12493=ORIENTED_EDGE ( 'NONE', *, *, #11847, .T. ) ;
#12513=CARTESIAN_POINT ( 'NONE',  ( 190.2689011420771976, 20.08915143297736350, -178.2104428091926991 ) ) ;
#12524=AXIS2_PLACEMENT_3D ( 'NONE', #3078, #7159, #97 ) ;
#12528=CARTESIAN_POINT ( 'NONE',  ( 159.3024069661366866, 19.96883746137792670, -207.6469600131167681 ) ) ;
#12539=FACE_OUTER_BOUND ( 'NONE', #11904, .T. ) ;
#12549=CARTESIAN_POINT ( 'NONE',  ( -252.9796497731091165, 20.55460285134058651, -67.76049180360037383 ) ) ;
#12581=CARTESIAN_POINT ( 'NONE',  ( 258.4638482596385529, 20.08915143297736350, 34.02434144668556115 ) ) ;
#12596=CARTESIAN_POINT ( 'NONE',  ( -1.008906662707803564E-12, 19.96883746059272724, 261.1558126970361400 ) ) ;
#12601=CARTESIAN_POINT ( 'NONE',  ( -260.1353576186481291, 20.08915143297736705, -17.05322212017824768 ) ) ;
#12614=CARTESIAN_POINT ( 'NONE',  ( 234.7354397747064354, 19.96883745941838484, 115.7315435904383349 ) ) ;
#12621=CARTESIAN_POINT ( 'NONE',  ( 42.50473797389777530, 20.79694577634646890, -257.4287020129718826 ) ) ;
#12638=AXIS2_PLACEMENT_3D ( 'NONE', #12095, #2954, #12035 ) ;
#12661=CARTESIAN_POINT ( 'NONE',  ( -226.6392846543355688, 19.96883746039994278, 130.8783844631124680 ) ) ;
#12664=CARTESIAN_POINT ( 'NONE',  ( -1.008906662707803362E-12, 19.96883746059273435, 261.1558126970361400 ) ) ;
#12666=CARTESIAN_POINT ( 'NONE',  ( -107.5873595010545500, 20.08915143297736705, 237.4577367525701845 ) ) ;
#12681=CARTESIAN_POINT ( 'NONE',  ( -17.06760680892479698, 20.79694577614318973, 260.7745447066434963 ) ) ;
#12688=CARTESIAN_POINT ( 'NONE',  ( 247.0684411393755795, 20.79694577634646535, -83.86521783953189413 ) ) ;
#12702=VERTEX_POINT ( 'NONE', #12924 ) ;
#12718=CARTESIAN_POINT ( 'NONE',  ( 259.4723857435292302, 19.96883745945557820, -34.18476129351679305 ) ) ;
#12731=ORIENTED_EDGE ( 'NONE', *, *, #5835, .F. ) ;
#12739=CARTESIAN_POINT ( 'NONE',  ( 172.6991790967991847, 20.55460285078499183, -196.8887528227133714 ) ) ;
#12759=CARTESIAN_POINT ( 'NONE',  ( -83.95474316008289861, 20.08915143298712280, -247.2466869553079789 ) ) ;
#12786=CARTESIAN_POINT ( 'NONE',  ( -84.14846197958475216, 19.96883746048893471, -247.8175805193368717 ) ) ;
#12790=CARTESIAN_POINT ( 'NONE',  ( -171.8850263962758902, 20.08915143297736705, 196.0019244007916370 ) ) ;
#12797=AXIS2_PLACEMENT_3D ( 'NONE', #1909, #6720, #4627 ) ;
#12808=CARTESIAN_POINT ( 'NONE',  ( 252.9796497720277841, 20.55460285096646089, 67.76049180220992696 ) ) ;
#12820=CARTESIAN_POINT ( 'NONE',  ( 115.3046144132251385, 20.08915143297736350, 233.8077470125392665 ) ) ;
#12827=CARTESIAN_POINT ( 'NONE',  ( 158.9353507265259964, 20.08915143275230974, -207.1687172319319927 ) ) ;
#12828=DIRECTION ( 'NONE',  ( 0.000000000000000000, -1.000000000000000000, 0.000000000000000000 ) ) ;
#12857=CARTESIAN_POINT ( 'NONE',  ( -226.7975291074607469, 20.55460285152577526, 130.9697226057901673 ) ) ;
#12867=( BOUNDED_CURVE ( )  B_SPLINE_CURVE ( 3, ( #5474, #8672, #9532, #4400 ),
 .UNSPECIFIED., .F., .F. ) 
 B_SPLINE_CURVE_WITH_KNOTS ( ( 4, 4 ),
 ( 0.000000000000000000, 1.000000000000000000 ),
 .UNSPECIFIED. ) 
 CURVE ( )  GEOMETRIC_REPRESENTATION_ITEM ( )  RATIONAL_B_SPLINE_CURVE ( ( 1.000000000000000000, 0.4027746460044325238, 0.4027746460044325238, 1.000000000000000000 ) ) 
 REPRESENTATION_ITEM ( '' )  );
#12877=CARTESIAN_POINT ( 'NONE',  ( -34.13493237021134519, 20.79694577641179620, -259.0935598599534728 ) ) ;
#12889=CARTESIAN_POINT ( 'NONE',  ( -7.780566028168587395E-13, 20.08915143297736350, 260.5542428351130866 ) ) ;
#12894=CARTESIAN_POINT ( 'NONE',  ( -17.05314194195814892, 20.08915143288246696, 260.5542428355875018 ) ) ;
#12909=CARTESIAN_POINT ( 'NONE',  ( -253.8843055347120412, 20.08915143297736705, 59.19439222780385279 ) ) ;
#12912=CARTESIAN_POINT ( 'NONE',  ( -17.06764083276443955, 20.79694577634646890, -260.3553053170167004 ) ) ;
#12921=CARTESIAN_POINT ( 'NONE',  ( 172.6991790967991847, 20.55460285078499183, -196.8887528227133714 ) ) ;
#12924=CARTESIAN_POINT ( 'NONE',  ( 3.012631125902489062E-14, 24.99999999999995737, 246.0000000000000000 ) ) ;
#12939=CARTESIAN_POINT ( 'NONE',  ( 226.7975291075301811, 20.55460285098495277, 130.9697226058104036 ) ) ;
#12958=CARTESIAN_POINT ( 'NONE',  ( -196.2980642837470100, 20.08915143287812199, -172.1812796682245050 ) ) ;
#12966=DIRECTION ( 'NONE',  ( 0.000000000000000000, 1.000000000000000000, 0.000000000000000000 ) ) ;
#12977=CARTESIAN_POINT ( 'NONE',  ( -7.780566028168587395E-13, 20.08915143297736350, 260.5542428351130866 ) ) ;
#12984=TOROIDAL_SURFACE ( 'NONE', #7020, 250.7029414592220178, 3.000000000000000000 ) ;
#12990=CARTESIAN_POINT ( 'NONE',  ( -247.9906035367588402, 20.55460285060343040, -84.20717312374212327 ) ) ;
#13006=PRODUCT_DEFINITION_FORMATION_WITH_SPECIFIED_SOURCE ( 'ANY', '', #439, .NOT_KNOWN. ) ;
#13010=CARTESIAN_POINT ( 'NONE',  ( 67.61424743001118998, 20.79694577617620155, -252.4341100437179648 ) ) ;
#13014=COLOUR_RGB ( '', 0.66274510, 0.83137255, 0.94901961) ;
#13025=CARTESIAN_POINT ( 'NONE',  ( -252.2208631662124958, 20.08915143301432948, -67.55708173888800161 ) ) ;
ENDSEC;
END-ISO-10303-21;
